ISO-10303-21;
HEADER;
/* Generated by software containing ST-Developer
 * from STEP Tools, Inc. (www.steptools.com) 
 */
/* OPTION: using custom renumber hook */

FILE_DESCRIPTION(
/* description */ ('STEP AP242 Edition 2', 'CAx-IF Rec.Pracs.---Representation and Presentation of Product Manufa
cturing Information (PMI)---4.0---2014-10-13', 'CAx-IF Rec.Pracs.---3D Tessellated Geometry---0.4---2014-09-14', '2;1', 'CAx-IF Rec.Pracs.---User Defined Attributes---1.5---2016-08-15'),
/* implementation_level */ '2;1');

FILE_NAME(
/* name */ 'Part 1__PD8596.step',
/* time_stamp */ '2026-10-07T00:00:55Z',
/* author */ (''),
/* organization */ (''),
/* preprocessor_version */ 'ST-DEVELOPER v20',
/* originating_system */ 'ONSHAPE BY PTC INC, 1.221',
/* authorisation */ '  ');

FILE_SCHEMA (('AP242_MANAGED_MODEL_BASED_3D_ENGINEERING_MIM_LF { 1 0 10303 442 3 1 4 }'));
ENDSEC;

DATA;
#15=SPHERICAL_SURFACE('',#4886,0.001);
#16=SPHERICAL_SURFACE('',#4890,0.001);
#17=SPHERICAL_SURFACE('',#4891,0.001);
#18=SPHERICAL_SURFACE('',#4895,0.001);
#19=SPHERICAL_SURFACE('',#4896,0.001);
#20=SPHERICAL_SURFACE('',#4900,0.001);
#21=SPHERICAL_SURFACE('',#4901,0.001);
#22=SPHERICAL_SURFACE('',#4905,0.001);
#23=SPHERICAL_SURFACE('',#4913,0.001);
#24=SPHERICAL_SURFACE('',#4915,0.001);
#25=SPHERICAL_SURFACE('',#4930,0.001);
#26=SPHERICAL_SURFACE('',#4932,0.001);
#27=(
BOUNDED_SURFACE()
B_SPLINE_SURFACE(3,2,((#7577,#7578,#7579),(#7580,#7581,#7582),(#7583,#7584,
#7585),(#7586,#7587,#7588)),.UNSPECIFIED.,.F.,.F.,.F.)
B_SPLINE_SURFACE_WITH_KNOTS((4,4),(3,3),(1.34441069388203E-17,0.00447796131591151),
(0.,1.),.PIECEWISE_BEZIER_KNOTS.)
GEOMETRIC_REPRESENTATION_ITEM()
RATIONAL_B_SPLINE_SURFACE(((1.,0.707106781186548,1.),(1.,0.71832066777653,
1.),(1.,0.718320667776528,1.),(1.,0.707106781186548,1.)))
REPRESENTATION_ITEM('')
SURFACE()
);
#28=(
BOUNDED_SURFACE()
B_SPLINE_SURFACE(3,2,((#7598,#7599,#7600),(#7601,#7602,#7603),(#7604,#7605,
#7606),(#7607,#7608,#7609),(#7610,#7611,#7612),(#7613,#7614,#7615)),
 .UNSPECIFIED.,.F.,.F.,.F.)
B_SPLINE_SURFACE_WITH_KNOTS((4,1,1,4),(3,3),(1.73472347597681E-18,0.00200651263897263,
0.00401302527794525,0.00802605055589049),(0.,1.),.UNSPECIFIED.)
GEOMETRIC_REPRESENTATION_ITEM()
RATIONAL_B_SPLINE_SURFACE(((1.,0.707106781186545,1.),(1.,0.714777484158914,
1.),(1.,0.738208449186217,1.),(1.,0.801379168437336,1.),(1.,0.836044012640875,
1.),(1.,0.836426120169544,1.)))
REPRESENTATION_ITEM('')
SURFACE()
);
#29=(
BOUNDED_SURFACE()
B_SPLINE_SURFACE(3,2,((#7635,#7636,#7637),(#7638,#7639,#7640),(#7641,#7642,
#7643),(#7644,#7645,#7646),(#7647,#7648,#7649),(#7650,#7651,#7652)),
 .UNSPECIFIED.,.F.,.F.,.F.)
B_SPLINE_SURFACE_WITH_KNOTS((4,1,1,4),(3,3),(-3.03576608295941E-18,0.00200651263897293,
0.00401302527794587,0.00802605055589175),(0.,1.),.UNSPECIFIED.)
GEOMETRIC_REPRESENTATION_ITEM()
RATIONAL_B_SPLINE_SURFACE(((1.,0.707106781186545,1.),(1.,0.714777484158915,
1.),(1.,0.738208449186387,1.),(1.,0.801379168436544,1.),(1.,0.836044012644433,
1.),(1.,0.836426120169542,1.)))
REPRESENTATION_ITEM('')
SURFACE()
);
#30=(
BOUNDED_SURFACE()
B_SPLINE_SURFACE(3,2,((#7656,#7657,#7658),(#7659,#7660,#7661),(#7662,#7663,
#7664),(#7665,#7666,#7667),(#7668,#7669,#7670)),.UNSPECIFIED.,.F.,.F.,.F.)
B_SPLINE_SURFACE_WITH_KNOTS((4,1,4),(3,3),(6.07153216591882E-18,0.00665411743559359,
0.0133082348711872),(0.,1.),.UNSPECIFIED.)
GEOMETRIC_REPRESENTATION_ITEM()
RATIONAL_B_SPLINE_SURFACE(((1.,0.707106781186547,1.),(1.,0.740921782108448,
1.),(1.,0.824106244556533,1.),(1.,0.890843705762328,1.),(1.,0.91150190641835,
1.)))
REPRESENTATION_ITEM('')
SURFACE()
);
#31=(
BOUNDED_SURFACE()
B_SPLINE_SURFACE(3,2,((#7679,#7680,#7681),(#7682,#7683,#7684),(#7685,#7686,
#7687),(#7688,#7689,#7690),(#7691,#7692,#7693),(#7694,#7695,#7696),(#7697,
#7698,#7699)),.UNSPECIFIED.,.F.,.F.,.F.)
B_SPLINE_SURFACE_WITH_KNOTS((4,1,1,1,4),(3,3),(1.21430643318376E-17,0.00345379209395837,
0.00690758418791672,0.0103613762818751,0.0138151683758334),(0.,1.),
 .UNSPECIFIED.)
GEOMETRIC_REPRESENTATION_ITEM()
RATIONAL_B_SPLINE_SURFACE(((1.,0.707106781186548,1.),(1.,0.723426406098682,
1.),(1.,0.760247481516635,1.),(1.,0.823847581524476,1.),(1.,0.886001526698892,
1.),(1.,0.919854499330898,1.),(1.,0.932470639919717,1.)))
REPRESENTATION_ITEM('')
SURFACE()
);
#32=(
BOUNDED_SURFACE()
B_SPLINE_SURFACE(3,2,((#7704,#7705,#7706),(#7707,#7708,#7709),(#7710,#7711,
#7712),(#7713,#7714,#7715),(#7716,#7717,#7718)),.UNSPECIFIED.,.F.,.F.,.F.)
B_SPLINE_SURFACE_WITH_KNOTS((4,1,4),(3,3),(6.07153216591882E-18,0.00665411743559357,
0.0133082348711871),(0.,1.),.UNSPECIFIED.)
GEOMETRIC_REPRESENTATION_ITEM()
RATIONAL_B_SPLINE_SURFACE(((1.,0.707106781186547,1.),(1.,0.740921782108448,
1.),(1.,0.824106244558266,1.),(1.,0.890843705758863,1.),(1.,0.91150190641835,
1.)))
REPRESENTATION_ITEM('')
SURFACE()
);
#33=(
BOUNDED_SURFACE()
B_SPLINE_SURFACE(3,2,((#7727,#7728,#7729),(#7730,#7731,#7732),(#7733,#7734,
#7735),(#7736,#7737,#7738),(#7739,#7740,#7741),(#7742,#7743,#7744),(#7745,
#7746,#7747)),.UNSPECIFIED.,.F.,.F.,.F.)
B_SPLINE_SURFACE_WITH_KNOTS((4,1,1,1,4),(3,3),(1.21430643318376E-17,0.00345379209395348,
0.00690758418790696,0.0103613762818604,0.0138151683758139),(0.,1.),
 .UNSPECIFIED.)
GEOMETRIC_REPRESENTATION_ITEM()
RATIONAL_B_SPLINE_SURFACE(((1.,0.707106781186548,1.),(1.,0.723426406098659,
1.),(1.,0.760247481516514,1.),(1.,0.823847581524435,1.),(1.,0.88600152669811,
1.),(1.,0.919854499331796,1.),(1.,0.932470639919502,1.)))
REPRESENTATION_ITEM('')
SURFACE()
);
#34=(
BOUNDED_SURFACE()
B_SPLINE_SURFACE(3,2,((#7762,#7763,#7764),(#7765,#7766,#7767),(#7768,#7769,
#7770),(#7771,#7772,#7773)),.UNSPECIFIED.,.F.,.F.,.F.)
B_SPLINE_SURFACE_WITH_KNOTS((4,4),(3,3),(-6.07153216591882E-18,0.00447796131591189),
(0.,1.),.PIECEWISE_BEZIER_KNOTS.)
GEOMETRIC_REPRESENTATION_ITEM()
RATIONAL_B_SPLINE_SURFACE(((1.,0.707106781186547,1.),(1.,0.718320667778804,
1.),(1.,0.718320667774086,1.),(1.,0.707106781186547,1.)))
REPRESENTATION_ITEM('')
SURFACE()
);
#35=(
BOUNDED_SURFACE()
B_SPLINE_SURFACE(3,2,((#7783,#7784,#7785),(#7786,#7787,#7788),(#7789,#7790,
#7791),(#7792,#7793,#7794),(#7795,#7796,#7797),(#7798,#7799,#7800)),
 .UNSPECIFIED.,.F.,.F.,.F.)
B_SPLINE_SURFACE_WITH_KNOTS((4,1,1,4),(3,3),(-6.07153216591882E-18,0.00200651263897325,
0.00401302527794651,0.00802605055589303),(0.,1.),.UNSPECIFIED.)
GEOMETRIC_REPRESENTATION_ITEM()
RATIONAL_B_SPLINE_SURFACE(((1.,0.707106781186545,1.),(1.,0.71477748415869,
1.),(1.,0.738208449186489,1.),(1.,0.801379168436508,1.),(1.,0.836044012644435,
1.),(1.,0.836426120169544,1.)))
REPRESENTATION_ITEM('')
SURFACE()
);
#36=(
BOUNDED_SURFACE()
B_SPLINE_SURFACE(3,2,((#7820,#7821,#7822),(#7823,#7824,#7825),(#7826,#7827,
#7828),(#7829,#7830,#7831),(#7832,#7833,#7834),(#7835,#7836,#7837)),
 .UNSPECIFIED.,.F.,.F.,.F.)
B_SPLINE_SURFACE_WITH_KNOTS((4,1,1,4),(3,3),(-3.46944695195361E-18,0.00200651263897327,
0.00401302527794655,0.0080260505558931),(0.,1.),.UNSPECIFIED.)
GEOMETRIC_REPRESENTATION_ITEM()
RATIONAL_B_SPLINE_SURFACE(((1.,0.707106781186545,1.),(1.,0.71477748415869,
1.),(1.,0.738208449186491,1.),(1.,0.80137916843651,1.),(1.,0.836044012644435,
1.),(1.,0.836426120169544,1.)))
REPRESENTATION_ITEM('')
SURFACE()
);
#37=(
BOUNDED_SURFACE()
B_SPLINE_SURFACE(3,2,((#7841,#7842,#7843),(#7844,#7845,#7846),(#7847,#7848,
#7849),(#7850,#7851,#7852),(#7853,#7854,#7855)),.UNSPECIFIED.,.F.,.F.,.F.)
B_SPLINE_SURFACE_WITH_KNOTS((4,1,4),(3,3),(-1.90819582357449E-17,0.00665411743559197,
0.013308234871184),(0.,1.),.UNSPECIFIED.)
GEOMETRIC_REPRESENTATION_ITEM()
RATIONAL_B_SPLINE_SURFACE(((1.,0.707106781186595,1.),(1.,0.740921782104245,
1.),(1.,0.824106244558438,1.),(1.,0.890843705762829,1.),(1.,0.911501906418351,
1.)))
REPRESENTATION_ITEM('')
SURFACE()
);
#38=(
BOUNDED_SURFACE()
B_SPLINE_SURFACE(3,2,((#7864,#7865,#7866),(#7867,#7868,#7869),(#7870,#7871,
#7872),(#7873,#7874,#7875),(#7876,#7877,#7878),(#7879,#7880,#7881),(#7882,
#7883,#7884)),.UNSPECIFIED.,.F.,.F.,.F.)
B_SPLINE_SURFACE_WITH_KNOTS((4,1,1,1,4),(3,3),(1.99493199737333E-17,0.00345379209395838,
0.00690758418791674,0.0103613762818751,0.0138151683758335),(0.,1.),
 .UNSPECIFIED.)
GEOMETRIC_REPRESENTATION_ITEM()
RATIONAL_B_SPLINE_SURFACE(((1.,0.707106781186548,1.),(1.,0.723426406098682,
1.),(1.,0.760247481516625,1.),(1.,0.823847581524508,1.),(1.,0.886001526698772,
1.),(1.,0.919854499331156,1.),(1.,0.932470639919717,1.)))
REPRESENTATION_ITEM('')
SURFACE()
);
#39=(
BOUNDED_SURFACE()
B_SPLINE_SURFACE(3,2,((#7889,#7890,#7891),(#7892,#7893,#7894),(#7895,#7896,
#7897),(#7898,#7899,#7900),(#7901,#7902,#7903)),.UNSPECIFIED.,.F.,.F.,.F.)
B_SPLINE_SURFACE_WITH_KNOTS((4,1,4),(3,3),(5.20417042793042E-18,0.0066541174355936,
0.0133082348711872),(0.,1.),.UNSPECIFIED.)
GEOMETRIC_REPRESENTATION_ITEM()
RATIONAL_B_SPLINE_SURFACE(((1.,0.707106781186548,1.),(1.,0.740921782105829,
1.),(1.,0.824106244557286,1.),(1.,0.890843705763443,1.),(1.,0.911501906418351,
1.)))
REPRESENTATION_ITEM('')
SURFACE()
);
#40=(
BOUNDED_SURFACE()
B_SPLINE_SURFACE(3,2,((#7912,#7913,#7914),(#7915,#7916,#7917),(#7918,#7919,
#7920),(#7921,#7922,#7923),(#7924,#7925,#7926),(#7927,#7928,#7929),(#7930,
#7931,#7932)),.UNSPECIFIED.,.F.,.F.,.F.)
B_SPLINE_SURFACE_WITH_KNOTS((4,1,1,1,4),(3,3),(8.67361737988404E-18,0.00345379209395273,
0.00690758418790545,0.0103613762818582,0.0138151683758109),(0.,1.),
 .UNSPECIFIED.)
GEOMETRIC_REPRESENTATION_ITEM()
RATIONAL_B_SPLINE_SURFACE(((1.,0.707106781186591,1.),(1.,0.723426406097336,
1.),(1.,0.760247481517187,1.),(1.,0.823847581524302,1.),(1.,0.886001526698139,
1.),(1.,0.919854499331863,1.),(1.,0.932470639919503,1.)))
REPRESENTATION_ITEM('')
SURFACE()
);
#123=SHAPE_REPRESENTATION_RELATIONSHIP('','',#4479,#134);
#134=ADVANCED_BREP_SHAPE_REPRESENTATION('',(#4455),#8542);
#144=TOROIDAL_SURFACE('',#4690,0.027,0.001);
#145=TOROIDAL_SURFACE('',#4691,0.027,0.001);
#146=TOROIDAL_SURFACE('',#4788,0.0232046666802154,0.01);
#147=TOROIDAL_SURFACE('',#4791,0.0232046666802154,0.01);
#148=TOROIDAL_SURFACE('',#4793,0.0232046666802154,0.01);
#149=TOROIDAL_SURFACE('',#4796,0.0232046666802154,0.01);
#150=TOROIDAL_SURFACE('',#4798,0.0381475271495645,0.01);
#151=TOROIDAL_SURFACE('',#4800,0.0381475271495645,0.01);
#152=TOROIDAL_SURFACE('',#4802,0.0104910488,0.001);
#153=TOROIDAL_SURFACE('',#4805,0.007207892,0.001);
#154=TOROIDAL_SURFACE('',#4812,0.0124910488,0.001);
#155=TOROIDAL_SURFACE('',#4816,0.009207892,0.001);
#156=TOROIDAL_SURFACE('',#4818,0.0124910488,0.001);
#157=TOROIDAL_SURFACE('',#4821,0.009207892,0.001);
#158=TOROIDAL_SURFACE('',#4823,0.0335028673605553,0.001);
#159=TOROIDAL_SURFACE('',#4828,0.0335028673605553,0.001);
#160=TOROIDAL_SURFACE('',#4832,0.0665016995023668,0.001);
#161=TOROIDAL_SURFACE('',#4835,0.0335028673605553,0.001);
#162=TOROIDAL_SURFACE('',#4840,0.0335028673605553,0.001);
#163=TOROIDAL_SURFACE('',#4844,0.0665016995023668,0.001);
#164=TOROIDAL_SURFACE('',#4847,0.0124910488,0.001);
#165=TOROIDAL_SURFACE('',#4851,0.009207892,0.001);
#166=TOROIDAL_SURFACE('',#4853,0.0124910488,0.001);
#167=TOROIDAL_SURFACE('',#4855,0.0174510516898875,0.0164511617441065);
#168=TOROIDAL_SURFACE('',#4856,0.009207892,0.001);
#169=TOROIDAL_SURFACE('',#4858,0.0335028673605553,0.001);
#170=TOROIDAL_SURFACE('',#4863,0.0335028673605553,0.001);
#171=TOROIDAL_SURFACE('',#4867,0.0665016995023668,0.001);
#172=TOROIDAL_SURFACE('',#4870,0.0335028673605553,0.001);
#173=TOROIDAL_SURFACE('',#4875,0.0335028673605553,0.001);
#174=TOROIDAL_SURFACE('',#4879,0.0665016995023668,0.001);
#175=TOROIDAL_SURFACE('',#4882,0.007207892,0.001);
#176=TOROIDAL_SURFACE('',#4885,0.0104910488,0.001);
#177=TOROIDAL_SURFACE('',#4888,0.030591099482527,0.001);
#178=TOROIDAL_SURFACE('',#4903,0.030591099482527,0.001);
#179=TOROIDAL_SURFACE('',#4906,0.0141998,0.001);
#180=TOROIDAL_SURFACE('',#4909,0.0665016995023668,0.001);
#181=TOROIDAL_SURFACE('',#4911,0.0665016995023668,0.001);
#182=TOROIDAL_SURFACE('',#4917,0.0147142518944256,0.001);
#183=TOROIDAL_SURFACE('',#4918,0.0147142518944256,0.001);
#184=TOROIDAL_SURFACE('',#4920,0.0132,0.001);
#185=TOROIDAL_SURFACE('',#4921,0.012,0.001);
#186=TOROIDAL_SURFACE('',#4922,0.012,0.001);
#187=TOROIDAL_SURFACE('',#4923,0.0141998,0.001);
#188=TOROIDAL_SURFACE('',#4926,0.0665016995023668,0.001);
#189=TOROIDAL_SURFACE('',#4928,0.0665016995023668,0.001);
#190=TOROIDAL_SURFACE('',#4934,0.0147142518944256,0.001);
#191=TOROIDAL_SURFACE('',#4935,0.0147142518944256,0.001);
#192=TOROIDAL_SURFACE('',#4937,0.0132,0.001);
#239=CYLINDRICAL_SURFACE('',#4663,0.024);
#240=CYLINDRICAL_SURFACE('',#4666,0.0045);
#241=CYLINDRICAL_SURFACE('',#4668,0.0045);
#242=CYLINDRICAL_SURFACE('',#4670,0.026);
#243=CYLINDRICAL_SURFACE('',#4674,0.026);
#244=CYLINDRICAL_SURFACE('',#4678,0.001);
#245=CYLINDRICAL_SURFACE('',#4681,0.001);
#246=CYLINDRICAL_SURFACE('',#4684,0.001);
#247=CYLINDRICAL_SURFACE('',#4687,0.001);
#248=CYLINDRICAL_SURFACE('',#4713,0.0655016995023668);
#249=CYLINDRICAL_SURFACE('',#4718,0.0655016995023668);
#250=CYLINDRICAL_SURFACE('',#4744,0.0325028673605553);
#251=CYLINDRICAL_SURFACE('',#4749,0.0151998);
#252=CYLINDRICAL_SURFACE('',#4752,0.0325028673605553);
#253=CYLINDRICAL_SURFACE('',#4759,0.011);
#254=CYLINDRICAL_SURFACE('',#4763,0.008207892);
#255=CYLINDRICAL_SURFACE('',#4768,0.0114910488);
#256=CYLINDRICAL_SURFACE('',#4776,0.0114910488);
#257=CYLINDRICAL_SURFACE('',#4781,0.008207892);
#258=CYLINDRICAL_SURFACE('',#4790,0.01);
#259=CYLINDRICAL_SURFACE('',#4795,0.01);
#260=CYLINDRICAL_SURFACE('',#4803,0.001);
#261=CYLINDRICAL_SURFACE('',#4804,0.001);
#262=CYLINDRICAL_SURFACE('',#4814,0.001);
#263=CYLINDRICAL_SURFACE('',#4819,0.001);
#264=CYLINDRICAL_SURFACE('',#4820,0.000999979135152545);
#265=CYLINDRICAL_SURFACE('',#4830,0.001);
#266=CYLINDRICAL_SURFACE('',#4842,0.001);
#267=CYLINDRICAL_SURFACE('',#4849,0.001);
#268=CYLINDRICAL_SURFACE('',#4854,0.001);
#269=CYLINDRICAL_SURFACE('',#4865,0.001);
#270=CYLINDRICAL_SURFACE('',#4877,0.001);
#271=CYLINDRICAL_SURFACE('',#4883,0.001);
#272=CYLINDRICAL_SURFACE('',#4884,0.001);
#273=CYLINDRICAL_SURFACE('',#4893,0.001);
#274=CYLINDRICAL_SURFACE('',#4898,0.001);
#275=CYLINDRICAL_SURFACE('',#4919,0.001);
#276=CYLINDRICAL_SURFACE('',#4936,0.001);
#374=CIRCLE('',#4652,0.027);
#375=CIRCLE('',#4653,0.0335028673605553);
#376=CIRCLE('',#4654,0.030591099482527);
#377=CIRCLE('',#4655,0.0335028673605553);
#378=CIRCLE('',#4657,0.0335028673605553);
#379=CIRCLE('',#4658,0.030591099482527);
#380=CIRCLE('',#4659,0.0335028673605553);
#381=CIRCLE('',#4660,0.027);
#382=CIRCLE('',#4664,0.024);
#383=CIRCLE('',#4665,0.024);
#384=CIRCLE('',#4667,0.0045);
#385=CIRCLE('',#4669,0.0045);
#386=CIRCLE('',#4671,0.026);
#387=CIRCLE('',#4672,0.026);
#388=CIRCLE('',#4675,0.026);
#389=CIRCLE('',#4676,0.026);
#390=CIRCLE('',#4679,0.001);
#391=CIRCLE('',#4680,0.001);
#392=CIRCLE('',#4682,0.001);
#393=CIRCLE('',#4683,0.001);
#394=CIRCLE('',#4685,0.001);
#395=CIRCLE('',#4686,0.001);
#396=CIRCLE('',#4688,0.001);
#397=CIRCLE('',#4689,0.001);
#398=CIRCLE('',#4693,0.009207892);
#399=CIRCLE('',#4694,0.0232046666802154);
#400=CIRCLE('',#4695,0.0665016995023668);
#401=CIRCLE('',#4696,0.0335028673605553);
#402=CIRCLE('',#4697,0.0381475271495645);
#403=CIRCLE('',#4698,0.0124910488);
#404=CIRCLE('',#4700,0.009207892);
#405=CIRCLE('',#4701,0.0232046666802154);
#406=CIRCLE('',#4702,0.0665016995023668);
#407=CIRCLE('',#4703,0.0335028673605553);
#408=CIRCLE('',#4704,0.0381475271495645);
#409=CIRCLE('',#4705,0.0124910488);
#410=CIRCLE('',#4707,0.0665016995023668);
#411=CIRCLE('',#4708,0.0147142518944256);
#412=CIRCLE('',#4709,0.0147142518944256);
#413=CIRCLE('',#4710,0.0665016995023668);
#414=CIRCLE('',#4711,0.0141998);
#415=CIRCLE('',#4712,0.0132);
#416=CIRCLE('',#4714,0.0655016995023668);
#417=CIRCLE('',#4715,0.0655016995023668);
#418=CIRCLE('',#4716,0.0655016995023668);
#419=CIRCLE('',#4717,0.0655016995023668);
#420=CIRCLE('',#4719,0.0655016995023668);
#421=CIRCLE('',#4720,0.0655016995023668);
#422=CIRCLE('',#4721,0.0655016995023668);
#423=CIRCLE('',#4722,0.0655016995023668);
#424=CIRCLE('',#4724,0.0665016995023668);
#425=CIRCLE('',#4725,0.0147142518944256);
#426=CIRCLE('',#4726,0.0147142518944256);
#427=CIRCLE('',#4727,0.0665016995023668);
#428=CIRCLE('',#4728,0.0141998);
#429=CIRCLE('',#4729,0.0132);
#430=CIRCLE('',#4731,0.0124910488);
#431=CIRCLE('',#4732,0.0381475271495645);
#432=CIRCLE('',#4733,0.0335028673605553);
#433=CIRCLE('',#4734,0.0665016995023668);
#434=CIRCLE('',#4735,0.0232046666802154);
#435=CIRCLE('',#4736,0.009207892);
#436=CIRCLE('',#4738,0.0124910488);
#437=CIRCLE('',#4739,0.0381475271495645);
#438=CIRCLE('',#4740,0.0335028673605553);
#439=CIRCLE('',#4741,0.0665016995023668);
#440=CIRCLE('',#4742,0.0232046666802154);
#441=CIRCLE('',#4743,0.009207892);
#442=CIRCLE('',#4745,0.0325028673605553);
#443=CIRCLE('',#4746,0.0325028673605553);
#444=CIRCLE('',#4747,0.0325028673605553);
#445=CIRCLE('',#4748,0.0325028673605553);
#446=CIRCLE('',#4750,0.0151998);
#447=CIRCLE('',#4751,0.0151998);
#448=CIRCLE('',#4753,0.0325028673605553);
#449=CIRCLE('',#4754,0.0325028673605553);
#450=CIRCLE('',#4755,0.0325028673605553);
#451=CIRCLE('',#4756,0.0325028673605553);
#452=CIRCLE('',#4760,0.011);
#453=CIRCLE('',#4761,0.011);
#454=CIRCLE('',#4764,0.008207892);
#455=CIRCLE('',#4765,0.008207892);
#456=CIRCLE('',#4766,0.008207892);
#457=CIRCLE('',#4769,0.0114910488);
#458=CIRCLE('',#4770,0.0114910488);
#459=CIRCLE('',#4771,0.0114910488);
#460=CIRCLE('',#4773,0.007207892);
#461=CIRCLE('',#4774,0.0104910488);
#462=CIRCLE('',#4777,0.0114910488);
#463=CIRCLE('',#4778,0.0114910488);
#464=CIRCLE('',#4779,0.0114910488);
#465=CIRCLE('',#4782,0.008207892);
#466=CIRCLE('',#4783,0.008207892);
#467=CIRCLE('',#4784,0.008207892);
#468=CIRCLE('',#4786,0.0104910488);
#469=CIRCLE('',#4787,0.007207892);
#470=CIRCLE('',#4789,0.0154861077840428);
#471=CIRCLE('',#4792,0.0154861077840428);
#472=CIRCLE('',#4794,0.0154861077840428);
#473=CIRCLE('',#4797,0.0154861077840428);
#474=CIRCLE('',#4799,0.0312780474522577);
#475=CIRCLE('',#4801,0.0312780474522577);
#476=CIRCLE('',#4807,0.012);
#477=CIRCLE('',#4808,0.0122);
#478=CIRCLE('',#4810,0.012);
#479=CIRCLE('',#4811,0.0122);
#480=CIRCLE('',#4813,0.001);
#481=CIRCLE('',#4815,0.001);
#482=CIRCLE('',#4817,0.001);
#483=CIRCLE('',#4822,0.001);
#484=CIRCLE('',#4824,0.001);
#485=CIRCLE('',#4825,0.001);
#486=CIRCLE('',#4826,0.001);
#487=CIRCLE('',#4827,0.001);
#488=CIRCLE('',#4829,0.001);
#489=CIRCLE('',#4831,0.001);
#490=CIRCLE('',#4833,0.001);
#491=CIRCLE('',#4834,0.001);
#492=CIRCLE('',#4836,0.001);
#493=CIRCLE('',#4837,0.001);
#494=CIRCLE('',#4838,0.001);
#495=CIRCLE('',#4839,0.001);
#496=CIRCLE('',#4841,0.001);
#497=CIRCLE('',#4843,0.001);
#498=CIRCLE('',#4845,0.001);
#499=CIRCLE('',#4846,0.001);
#500=CIRCLE('',#4848,0.001);
#501=CIRCLE('',#4850,0.001);
#502=CIRCLE('',#4852,0.001);
#503=CIRCLE('',#4857,0.001);
#504=CIRCLE('',#4859,0.001);
#505=CIRCLE('',#4860,0.001);
#506=CIRCLE('',#4861,0.001);
#507=CIRCLE('',#4862,0.001);
#508=CIRCLE('',#4864,0.001);
#509=CIRCLE('',#4866,0.001);
#510=CIRCLE('',#4868,0.001);
#511=CIRCLE('',#4869,0.001);
#512=CIRCLE('',#4871,0.001);
#513=CIRCLE('',#4872,0.001);
#514=CIRCLE('',#4873,0.001);
#515=CIRCLE('',#4874,0.001);
#516=CIRCLE('',#4876,0.001);
#517=CIRCLE('',#4878,0.001);
#518=CIRCLE('',#4880,0.001);
#519=CIRCLE('',#4881,0.001);
#520=CIRCLE('',#4887,0.001);
#521=CIRCLE('',#4889,0.001);
#522=CIRCLE('',#4892,0.001);
#523=CIRCLE('',#4894,0.001);
#524=CIRCLE('',#4897,0.001);
#525=CIRCLE('',#4899,0.001);
#526=CIRCLE('',#4902,0.001);
#527=CIRCLE('',#4904,0.001);
#528=CIRCLE('',#4907,0.001);
#529=CIRCLE('',#4908,0.001);
#530=CIRCLE('',#4910,0.001);
#531=CIRCLE('',#4912,0.001);
#532=CIRCLE('',#4914,0.001);
#533=CIRCLE('',#4916,0.001);
#534=CIRCLE('',#4924,0.001);
#535=CIRCLE('',#4925,0.001);
#536=CIRCLE('',#4927,0.001);
#537=CIRCLE('',#4929,0.001);
#538=CIRCLE('',#4931,0.001);
#539=CIRCLE('',#4933,0.001);
#607=B_SPLINE_CURVE_WITH_KNOTS('',3,(#6965,#6966,#6967,#6968,#6969,#6970,
#6971,#6972,#6973,#6974,#6975,#6976,#6977,#6978,#6979,#6980,#6981,#6982,
#6983),.UNSPECIFIED.,.T.,.F.,(1,1,1,1,1,1,1,1,1,1,1,1,1,1,1,1,1,1,1,1,1,
1,1),(-0.00575205114744636,-0.00383470076496424,-0.00191735038248212,0.,
0.00191735038248212,0.00383470076496424,0.00575205114744636,0.00766940152992848,
0.0095867519124106,0.0115041022948927,0.0134214526773748,0.015338803059857,
0.0172561534423391,0.0191735038248212,0.0210908542073033,0.0230082045897854,
0.0249255549722676,0.0268429053547497,0.0287602557372318,0.0306776061197139,
0.032594956502196,0.0345123068846782,0.0364296572671603),.UNSPECIFIED.);
#608=B_SPLINE_CURVE_WITH_KNOTS('',3,(#6988,#6989,#6990,#6991,#6992,#6993,
#6994,#6995,#6996,#6997,#6998,#6999,#7000,#7001,#7002,#7003,#7004,#7005,
#7006),.UNSPECIFIED.,.T.,.F.,(1,1,1,1,1,1,1,1,1,1,1,1,1,1,1,1,1,1,1,1,1,
1,1),(-0.00575205114744637,-0.00383470076496424,-0.00191735038248212,0.,
0.00191735038248212,0.00383470076496425,0.00575205114744637,0.00766940152992849,
0.00958675191241062,0.0115041022948927,0.0134214526773749,0.015338803059857,
0.0172561534423391,0.0191735038248212,0.0210908542073034,0.0230082045897855,
0.0249255549722676,0.0268429053547497,0.0287602557372319,0.030677606119714,
0.0325949565021961,0.0345123068846782,0.0364296572671603),.UNSPECIFIED.);
#609=B_SPLINE_CURVE_WITH_KNOTS('',3,(#7047,#7048,#7049,#7050,#7051),
 .UNSPECIFIED.,.F.,.F.,(4,1,4),(0.00437149970837484,0.00516403730127254,
0.00595657489417023),.UNSPECIFIED.);
#610=B_SPLINE_CURVE_WITH_KNOTS('',3,(#7052,#7053,#7054,#7055,#7056),
 .UNSPECIFIED.,.F.,.F.,(4,1,4),(0.00493537550573997,0.00572807532890887,
0.00652077515207777),.UNSPECIFIED.);
#611=B_SPLINE_CURVE_WITH_KNOTS('',3,(#7058,#7059,#7060,#7061,#7062),
 .UNSPECIFIED.,.F.,.F.,(4,1,4),(0.000383476419715099,0.00117659400994475,
0.00196971160017441),.UNSPECIFIED.);
#612=B_SPLINE_CURVE_WITH_KNOTS('',3,(#7063,#7064,#7065,#7066,#7067),
 .UNSPECIFIED.,.F.,.F.,(4,1,4),(0.00616146542423319,0.00695359511819705,
0.0077457248121609),.UNSPECIFIED.);
#613=B_SPLINE_CURVE_WITH_KNOTS('',3,(#7123,#7124,#7125,#7126,#7127,#7128,
#7129),.UNSPECIFIED.,.F.,.F.,(4,1,1,1,4),(0.00352549128828216,0.00696797821694395,
0.0104104651456057,0.0138529520742675,0.0172954390029293),.UNSPECIFIED.);
#614=B_SPLINE_CURVE_WITH_KNOTS('',3,(#7137,#7138,#7139,#7140,#7141,#7142,
#7143),.UNSPECIFIED.,.F.,.F.,(4,1,1,1,4),(0.,0.00340629880233305,0.0068125976046661,
0.0102188964069992,0.0136251952093322),.UNSPECIFIED.);
#615=B_SPLINE_CURVE_WITH_KNOTS('',3,(#7147,#7148,#7149,#7150,#7151,#7152,
#7153),.UNSPECIFIED.,.F.,.F.,(4,1,1,1,4),(0.,0.00340629880233381,0.00681259760466761,
0.0102188964070014,0.0136251952093352),.UNSPECIFIED.);
#616=B_SPLINE_CURVE_WITH_KNOTS('',3,(#7162,#7163,#7164,#7165,#7166,#7167,
#7168),.UNSPECIFIED.,.F.,.F.,(4,1,1,1,4),(0.00352549128828207,0.00696797821694389,
0.0104104651456057,0.0138529520742675,0.0172954390029293),.UNSPECIFIED.);
#617=B_SPLINE_CURVE_WITH_KNOTS('',3,(#7232,#7233,#7234,#7235,#7236),
 .UNSPECIFIED.,.F.,.F.,(4,1,4),(0.,0.0064793361194087,0.0129586722388174),
 .UNSPECIFIED.);
#618=B_SPLINE_CURVE_WITH_KNOTS('',3,(#7244,#7245,#7246,#7247,#7248),
 .UNSPECIFIED.,.F.,.F.,(4,1,4),(0.,0.00645902084593716,0.0129180416918743),
 .UNSPECIFIED.);
#619=B_SPLINE_CURVE_WITH_KNOTS('',3,(#7260,#7261,#7262,#7263,#7264),
 .UNSPECIFIED.,.F.,.F.,(4,1,4),(0.,0.00647933611940867,0.0129586722388173),
 .UNSPECIFIED.);
#620=B_SPLINE_CURVE_WITH_KNOTS('',3,(#7272,#7273,#7274,#7275,#7276),
 .UNSPECIFIED.,.F.,.F.,(4,1,4),(0.,0.00645902084593563,0.0129180416918713),
 .UNSPECIFIED.);
#621=B_SPLINE_CURVE_WITH_KNOTS('',3,(#7298,#7299,#7300,#7301),
 .UNSPECIFIED.,.F.,.F.,(4,4),(8.13151629364128E-20,0.00716108843954949),
 .UNSPECIFIED.);
#622=B_SPLINE_CURVE_WITH_KNOTS('',3,(#7311,#7312,#7313,#7314),
 .UNSPECIFIED.,.F.,.F.,(4,4),(0.,0.00710594861592948),.UNSPECIFIED.);
#623=B_SPLINE_CURVE_WITH_KNOTS('',3,(#7316,#7317,#7318,#7319),
 .UNSPECIFIED.,.F.,.F.,(4,4),(0.,1.),.UNSPECIFIED.);
#624=B_SPLINE_CURVE_WITH_KNOTS('',3,(#7329,#7330,#7331,#7332),
 .UNSPECIFIED.,.F.,.F.,(4,4),(0.,0.00411946769479083),.UNSPECIFIED.);
#625=B_SPLINE_CURVE_WITH_KNOTS('',3,(#7360,#7361,#7362,#7363),
 .UNSPECIFIED.,.F.,.F.,(4,4),(0.,0.00411946769479048),.UNSPECIFIED.);
#626=B_SPLINE_CURVE_WITH_KNOTS('',3,(#7374,#7375,#7376,#7377),
 .UNSPECIFIED.,.F.,.F.,(4,4),(1.35525271560688E-20,0.00716108843954742),
 .UNSPECIFIED.);
#627=B_SPLINE_CURVE_WITH_KNOTS('',3,(#7384,#7385,#7386,#7387),
 .UNSPECIFIED.,.F.,.F.,(4,4),(0.,0.00710594861592814),.UNSPECIFIED.);
#628=B_SPLINE_CURVE_WITH_KNOTS('',3,(#7389,#7390,#7391,#7392),
 .UNSPECIFIED.,.F.,.F.,(4,4),(0.,1.),.UNSPECIFIED.);
#629=B_SPLINE_CURVE_WITH_KNOTS('',3,(#7403,#7404,#7405,#7406),
 .UNSPECIFIED.,.F.,.F.,(4,4),(0.000458247724612459,0.00515055882881692),
 .UNSPECIFIED.);
#630=B_SPLINE_CURVE_WITH_KNOTS('',3,(#7411,#7412,#7413,#7414,#7415,#7416),
 .UNSPECIFIED.,.F.,.F.,(4,1,1,4),(0.00143499903345957,0.00481436180627339,
0.00819372457908721,0.0149524501247149),.UNSPECIFIED.);
#631=B_SPLINE_CURVE_WITH_KNOTS('',3,(#7417,#7418,#7419,#7420,#7421),
 .UNSPECIFIED.,.F.,.F.,(4,1,4),(0.,0.00387944920372668,0.00775889840745336),
 .UNSPECIFIED.);
#632=B_SPLINE_CURVE_WITH_KNOTS('',3,(#7423,#7424,#7425,#7426),
 .UNSPECIFIED.,.F.,.F.,(4,4),(0.000458247724612459,0.00515055882881692),
 .UNSPECIFIED.);
#633=B_SPLINE_CURVE_WITH_KNOTS('',3,(#7430,#7431,#7432,#7433),
 .UNSPECIFIED.,.F.,.F.,(4,4),(0.,1.),.UNSPECIFIED.);
#634=B_SPLINE_CURVE_WITH_KNOTS('',3,(#7435,#7436,#7437,#7438,#7439,#7440),
 .UNSPECIFIED.,.F.,.F.,(4,1,1,4),(0.,0.00671446169703845,0.0100716925455577,
0.0134289233940769),.UNSPECIFIED.);
#635=B_SPLINE_CURVE_WITH_KNOTS('',3,(#7443,#7444,#7445,#7446,#7447),
 .UNSPECIFIED.,.F.,.F.,(4,1,4),(0.,0.00391314275686453,0.00782628551372907),
 .UNSPECIFIED.);
#636=B_SPLINE_CURVE_WITH_KNOTS('',3,(#7449,#7450,#7451,#7452),
 .UNSPECIFIED.,.F.,.F.,(4,4),(0.000458247724612439,0.00515055882881691),
 .UNSPECIFIED.);
#637=B_SPLINE_CURVE_WITH_KNOTS('',3,(#7457,#7458,#7459,#7460,#7461,#7462),
 .UNSPECIFIED.,.F.,.F.,(4,1,1,4),(0.00143499903345957,0.00481436180627316,
0.00819372457908675,0.0149524501247139),.UNSPECIFIED.);
#638=B_SPLINE_CURVE_WITH_KNOTS('',3,(#7463,#7464,#7465,#7466,#7467),
 .UNSPECIFIED.,.F.,.F.,(4,1,4),(0.,0.00387944920372737,0.00775889840745473),
 .UNSPECIFIED.);
#639=B_SPLINE_CURVE_WITH_KNOTS('',3,(#7469,#7470,#7471,#7472),
 .UNSPECIFIED.,.F.,.F.,(4,4),(0.000458247724612439,0.00515055882881689),
 .UNSPECIFIED.);
#640=B_SPLINE_CURVE_WITH_KNOTS('',3,(#7476,#7477,#7478,#7479),
 .UNSPECIFIED.,.F.,.F.,(4,4),(0.,1.),.UNSPECIFIED.);
#641=B_SPLINE_CURVE_WITH_KNOTS('',3,(#7481,#7482,#7483,#7484,#7485,#7486),
 .UNSPECIFIED.,.F.,.F.,(4,1,1,4),(0.,0.00671446169703849,0.0100716925455577,
0.013428923394077),.UNSPECIFIED.);
#642=B_SPLINE_CURVE_WITH_KNOTS('',3,(#7489,#7490,#7491,#7492,#7493),
 .UNSPECIFIED.,.F.,.F.,(4,1,4),(0.,0.00391314275686577,0.00782628551373154),
 .UNSPECIFIED.);
#643=B_SPLINE_CURVE_WITH_KNOTS('',3,(#7495,#7496,#7497,#7498,#7499),
 .UNSPECIFIED.,.F.,.F.,(4,1,4),(0.,0.00647222827986434,0.0129444565597287),
 .UNSPECIFIED.);
#644=B_SPLINE_CURVE_WITH_KNOTS('',3,(#7503,#7504,#7505,#7506,#7507),
 .UNSPECIFIED.,.F.,.F.,(4,1,4),(0.00137904255227218,0.00786045945981697,
0.0143418763673618),.UNSPECIFIED.);
#645=B_SPLINE_CURVE_WITH_KNOTS('',3,(#7508,#7509,#7510,#7511),
 .UNSPECIFIED.,.F.,.F.,(4,4),(0.,0.00447796131591151),.UNSPECIFIED.);
#646=B_SPLINE_CURVE_WITH_KNOTS('',3,(#7513,#7514,#7515,#7516,#7517),
 .UNSPECIFIED.,.F.,.F.,(4,1,4),(0.,0.00647222827986436,0.0129444565597287),
 .UNSPECIFIED.);
#647=B_SPLINE_CURVE_WITH_KNOTS('',3,(#7521,#7522,#7523,#7524,#7525),
 .UNSPECIFIED.,.F.,.F.,(4,1,4),(0.00137904255227228,0.00786045945981642,
0.0143418763673606),.UNSPECIFIED.);
#648=B_SPLINE_CURVE_WITH_KNOTS('',3,(#7526,#7527,#7528,#7529),
 .UNSPECIFIED.,.F.,.F.,(4,4),(0.,0.00447796131591189),.UNSPECIFIED.);
#649=B_SPLINE_CURVE_WITH_KNOTS('',3,(#7531,#7532,#7533,#7534,#7535),
 .UNSPECIFIED.,.F.,.F.,(4,1,4),(0.,0.000781285135510639,0.00156257027102128),
 .UNSPECIFIED.);
#650=B_SPLINE_CURVE_WITH_KNOTS('',3,(#7536,#7537,#7538,#7539,#7540),
 .UNSPECIFIED.,.F.,.F.,(4,1,4),(0.,0.000781285135510629,0.00156257027102126),
 .UNSPECIFIED.);
#651=B_SPLINE_CURVE_WITH_KNOTS('',3,(#7542,#7543,#7544,#7545,#7546),
 .UNSPECIFIED.,.F.,.F.,(4,1,4),(0.,0.000781288146365363,0.00156257629273073),
 .UNSPECIFIED.);
#652=B_SPLINE_CURVE_WITH_KNOTS('',3,(#7548,#7549,#7550,#7551,#7552),
 .UNSPECIFIED.,.F.,.F.,(4,1,4),(0.,0.000781288146365363,0.00156257629273073),
 .UNSPECIFIED.);
#653=B_SPLINE_CURVE_WITH_KNOTS('',3,(#7566,#7567,#7568,#7569,#7570),
 .UNSPECIFIED.,.F.,.F.,(4,1,4),(0.,0.000781272382823816,0.00156254476564763),
 .UNSPECIFIED.);
#654=B_SPLINE_CURVE_WITH_KNOTS('',3,(#7572,#7573,#7574,#7575,#7576),
 .UNSPECIFIED.,.F.,.F.,(4,1,4),(0.,0.000781270211991802,0.0015625404239836),
 .UNSPECIFIED.);
#655=B_SPLINE_CURVE_WITH_KNOTS('',3,(#7593,#7594,#7595,#7596,#7597),
 .UNSPECIFIED.,.F.,.F.,(4,1,4),(0.,0.000781272382824027,0.00156254476564805),
 .UNSPECIFIED.);
#656=B_SPLINE_CURVE_WITH_KNOTS('',3,(#7616,#7617,#7618,#7619,#7620),
 .UNSPECIFIED.,.F.,.F.,(4,1,4),(0.,0.5,1.),.UNSPECIFIED.);
#657=B_SPLINE_CURVE_WITH_KNOTS('',3,(#7622,#7623,#7624,#7625,#7626),
 .UNSPECIFIED.,.F.,.F.,(4,1,4),(0.,0.000781270211991983,0.00156254042398397),
 .UNSPECIFIED.);
#658=B_SPLINE_CURVE_WITH_KNOTS('',3,(#7628,#7629,#7630,#7631,#7632),
 .UNSPECIFIED.,.F.,.F.,(4,1,4),(0.,0.5,1.),.UNSPECIFIED.);
#659=B_SPLINE_CURVE_WITH_KNOTS('',3,(#7751,#7752,#7753,#7754,#7755),
 .UNSPECIFIED.,.F.,.F.,(4,1,4),(0.,0.000781272382823819,0.00156254476564764),
 .UNSPECIFIED.);
#660=B_SPLINE_CURVE_WITH_KNOTS('',3,(#7757,#7758,#7759,#7760,#7761),
 .UNSPECIFIED.,.F.,.F.,(4,1,4),(0.,0.000781270211991816,0.00156254042398363),
 .UNSPECIFIED.);
#661=B_SPLINE_CURVE_WITH_KNOTS('',3,(#7778,#7779,#7780,#7781,#7782),
 .UNSPECIFIED.,.F.,.F.,(4,1,4),(0.,0.000781272382824017,0.00156254476564803),
 .UNSPECIFIED.);
#662=B_SPLINE_CURVE_WITH_KNOTS('',3,(#7801,#7802,#7803,#7804,#7805),
 .UNSPECIFIED.,.F.,.F.,(4,1,4),(0.,0.5,1.),.UNSPECIFIED.);
#663=B_SPLINE_CURVE_WITH_KNOTS('',3,(#7807,#7808,#7809,#7810,#7811),
 .UNSPECIFIED.,.F.,.F.,(4,1,4),(0.,0.000781270211991975,0.00156254042398395),
 .UNSPECIFIED.);
#664=B_SPLINE_CURVE_WITH_KNOTS('',3,(#7813,#7814,#7815,#7816,#7817),
 .UNSPECIFIED.,.F.,.F.,(4,1,4),(0.,0.5,1.),.UNSPECIFIED.);
#665=B_SPLINE_CURVE_WITH_KNOTS('',3,(#7935,#7936,#7937,#7938,#7939),
 .UNSPECIFIED.,.F.,.F.,(4,1,4),(0.,0.000781288146365333,0.00156257629273067),
 .UNSPECIFIED.);
#666=B_SPLINE_CURVE_WITH_KNOTS('',3,(#7940,#7941,#7942,#7943,#7944),
 .UNSPECIFIED.,.F.,.F.,(4,1,4),(0.,0.000781288146365363,0.00156257629273073),
 .UNSPECIFIED.);
#667=B_SPLINE_CURVE_WITH_KNOTS('',3,(#7946,#7947,#7948,#7949,#7950),
 .UNSPECIFIED.,.F.,.F.,(4,1,4),(0.,0.000781285135510639,0.00156257027102128),
 .UNSPECIFIED.);
#668=B_SPLINE_CURVE_WITH_KNOTS('',3,(#7952,#7953,#7954,#7955,#7956),
 .UNSPECIFIED.,.F.,.F.,(4,1,4),(0.,0.000781285135510639,0.00156257027102128),
 .UNSPECIFIED.);
#669=B_SPLINE_CURVE_WITH_KNOTS('',3,(#7990,#7991,#7992,#7993),
 .UNSPECIFIED.,.F.,.F.,(4,4),(1.11076830053021E-17,0.000876980038522517),
 .UNSPECIFIED.);
#670=B_SPLINE_CURVE_WITH_KNOTS('',3,(#7995,#7996,#7997,#7998),
 .UNSPECIFIED.,.F.,.F.,(4,4),(1.11076830053021E-17,0.000876980038522516),
 .UNSPECIFIED.);
#671=B_SPLINE_CURVE_WITH_KNOTS('',3,(#8015,#8016,#8017,#8018),
 .UNSPECIFIED.,.F.,.F.,(4,4),(0.,0.000876980038522527),.UNSPECIFIED.);
#672=B_SPLINE_CURVE_WITH_KNOTS('',3,(#8020,#8021,#8022,#8023),
 .UNSPECIFIED.,.F.,.F.,(4,4),(0.,0.000876980038522527),.UNSPECIFIED.);
#999=ORIENTED_EDGE('',*,*,#2019,.T.);
#1000=ORIENTED_EDGE('',*,*,#2020,.T.);
#1001=ORIENTED_EDGE('',*,*,#2021,.T.);
#1002=ORIENTED_EDGE('',*,*,#2022,.T.);
#1003=ORIENTED_EDGE('',*,*,#2023,.T.);
#1004=ORIENTED_EDGE('',*,*,#2024,.T.);
#1005=ORIENTED_EDGE('',*,*,#2025,.T.);
#1006=ORIENTED_EDGE('',*,*,#2026,.T.);
#1007=ORIENTED_EDGE('',*,*,#2027,.F.);
#1008=ORIENTED_EDGE('',*,*,#2028,.T.);
#1009=ORIENTED_EDGE('',*,*,#2029,.T.);
#1010=ORIENTED_EDGE('',*,*,#2030,.T.);
#1011=ORIENTED_EDGE('',*,*,#2031,.T.);
#1012=ORIENTED_EDGE('',*,*,#2032,.T.);
#1013=ORIENTED_EDGE('',*,*,#2033,.F.);
#1014=ORIENTED_EDGE('',*,*,#2034,.T.);
#1015=ORIENTED_EDGE('',*,*,#2035,.F.);
#1016=ORIENTED_EDGE('',*,*,#2036,.T.);
#1017=ORIENTED_EDGE('',*,*,#2037,.T.);
#1018=ORIENTED_EDGE('',*,*,#2038,.T.);
#1019=ORIENTED_EDGE('',*,*,#2039,.T.);
#1020=ORIENTED_EDGE('',*,*,#2040,.T.);
#1021=ORIENTED_EDGE('',*,*,#2041,.T.);
#1022=ORIENTED_EDGE('',*,*,#2042,.T.);
#1023=ORIENTED_EDGE('',*,*,#2043,.F.);
#1024=ORIENTED_EDGE('',*,*,#2044,.T.);
#1025=ORIENTED_EDGE('',*,*,#2045,.F.);
#1026=ORIENTED_EDGE('',*,*,#2046,.F.);
#1027=ORIENTED_EDGE('',*,*,#2047,.T.);
#1028=ORIENTED_EDGE('',*,*,#2048,.F.);
#1029=ORIENTED_EDGE('',*,*,#2049,.F.);
#1030=ORIENTED_EDGE('',*,*,#2050,.F.);
#1031=ORIENTED_EDGE('',*,*,#2051,.F.);
#1032=ORIENTED_EDGE('',*,*,#2052,.F.);
#1033=ORIENTED_EDGE('',*,*,#2053,.F.);
#1034=ORIENTED_EDGE('',*,*,#2054,.T.);
#1035=ORIENTED_EDGE('',*,*,#2052,.T.);
#1036=ORIENTED_EDGE('',*,*,#2055,.T.);
#1037=ORIENTED_EDGE('',*,*,#2044,.F.);
#1038=ORIENTED_EDGE('',*,*,#2056,.T.);
#1039=ORIENTED_EDGE('',*,*,#2057,.T.);
#1040=ORIENTED_EDGE('',*,*,#2058,.T.);
#1041=ORIENTED_EDGE('',*,*,#2059,.T.);
#1042=ORIENTED_EDGE('',*,*,#2060,.T.);
#1043=ORIENTED_EDGE('',*,*,#2059,.F.);
#1044=ORIENTED_EDGE('',*,*,#2061,.T.);
#1045=ORIENTED_EDGE('',*,*,#2046,.T.);
#1046=ORIENTED_EDGE('',*,*,#2062,.T.);
#1047=ORIENTED_EDGE('',*,*,#2023,.F.);
#1048=ORIENTED_EDGE('',*,*,#2063,.T.);
#1049=ORIENTED_EDGE('',*,*,#2039,.F.);
#1050=ORIENTED_EDGE('',*,*,#2064,.T.);
#1051=ORIENTED_EDGE('',*,*,#2041,.F.);
#1052=ORIENTED_EDGE('',*,*,#2065,.T.);
#1053=ORIENTED_EDGE('',*,*,#2032,.F.);
#1054=ORIENTED_EDGE('',*,*,#2066,.T.);
#1055=ORIENTED_EDGE('',*,*,#2036,.F.);
#1056=ORIENTED_EDGE('',*,*,#2067,.T.);
#1057=ORIENTED_EDGE('',*,*,#2019,.F.);
#1058=ORIENTED_EDGE('',*,*,#2068,.F.);
#1059=ORIENTED_EDGE('',*,*,#2028,.F.);
#1060=ORIENTED_EDGE('',*,*,#2069,.T.);
#1061=ORIENTED_EDGE('',*,*,#2038,.F.);
#1062=ORIENTED_EDGE('',*,*,#2070,.F.);
#1063=ORIENTED_EDGE('',*,*,#2071,.F.);
#1064=ORIENTED_EDGE('',*,*,#2054,.F.);
#1065=ORIENTED_EDGE('',*,*,#2072,.F.);
#1066=ORIENTED_EDGE('',*,*,#2034,.F.);
#1067=ORIENTED_EDGE('',*,*,#2073,.F.);
#1068=ORIENTED_EDGE('',*,*,#2021,.F.);
#1069=ORIENTED_EDGE('',*,*,#2074,.F.);
#1070=ORIENTED_EDGE('',*,*,#2057,.F.);
#1071=ORIENTED_EDGE('',*,*,#2075,.T.);
#1072=ORIENTED_EDGE('',*,*,#2076,.T.);
#1073=ORIENTED_EDGE('',*,*,#2077,.T.);
#1074=ORIENTED_EDGE('',*,*,#2078,.T.);
#1075=ORIENTED_EDGE('',*,*,#2079,.T.);
#1076=ORIENTED_EDGE('',*,*,#2080,.T.);
#1077=ORIENTED_EDGE('',*,*,#2081,.T.);
#1078=ORIENTED_EDGE('',*,*,#2082,.T.);
#1079=ORIENTED_EDGE('',*,*,#2083,.T.);
#1080=ORIENTED_EDGE('',*,*,#2084,.T.);
#1081=ORIENTED_EDGE('',*,*,#2085,.T.);
#1082=ORIENTED_EDGE('',*,*,#2086,.T.);
#1083=ORIENTED_EDGE('',*,*,#2087,.T.);
#1084=ORIENTED_EDGE('',*,*,#2088,.T.);
#1085=ORIENTED_EDGE('',*,*,#2089,.T.);
#1086=ORIENTED_EDGE('',*,*,#2090,.T.);
#1087=ORIENTED_EDGE('',*,*,#2091,.T.);
#1088=ORIENTED_EDGE('',*,*,#2092,.T.);
#1089=ORIENTED_EDGE('',*,*,#2093,.T.);
#1090=ORIENTED_EDGE('',*,*,#2094,.T.);
#1091=ORIENTED_EDGE('',*,*,#2095,.T.);
#1092=ORIENTED_EDGE('',*,*,#2096,.T.);
#1093=ORIENTED_EDGE('',*,*,#2097,.T.);
#1094=ORIENTED_EDGE('',*,*,#2098,.F.);
#1095=ORIENTED_EDGE('',*,*,#2099,.T.);
#1096=ORIENTED_EDGE('',*,*,#2100,.T.);
#1097=ORIENTED_EDGE('',*,*,#2101,.T.);
#1098=ORIENTED_EDGE('',*,*,#2102,.T.);
#1099=ORIENTED_EDGE('',*,*,#2103,.T.);
#1100=ORIENTED_EDGE('',*,*,#2104,.T.);
#1101=ORIENTED_EDGE('',*,*,#2105,.T.);
#1102=ORIENTED_EDGE('',*,*,#2106,.T.);
#1103=ORIENTED_EDGE('',*,*,#2107,.T.);
#1104=ORIENTED_EDGE('',*,*,#2108,.T.);
#1105=ORIENTED_EDGE('',*,*,#2109,.T.);
#1106=ORIENTED_EDGE('',*,*,#2110,.T.);
#1107=ORIENTED_EDGE('',*,*,#2111,.T.);
#1108=ORIENTED_EDGE('',*,*,#2112,.F.);
#1109=ORIENTED_EDGE('',*,*,#2113,.T.);
#1110=ORIENTED_EDGE('',*,*,#2114,.T.);
#1111=ORIENTED_EDGE('',*,*,#2115,.T.);
#1112=ORIENTED_EDGE('',*,*,#2116,.T.);
#1113=ORIENTED_EDGE('',*,*,#2117,.T.);
#1114=ORIENTED_EDGE('',*,*,#2118,.T.);
#1115=ORIENTED_EDGE('',*,*,#2119,.T.);
#1116=ORIENTED_EDGE('',*,*,#2120,.T.);
#1117=ORIENTED_EDGE('',*,*,#2121,.T.);
#1118=ORIENTED_EDGE('',*,*,#2122,.T.);
#1119=ORIENTED_EDGE('',*,*,#2123,.T.);
#1120=ORIENTED_EDGE('',*,*,#2124,.T.);
#1121=ORIENTED_EDGE('',*,*,#2125,.T.);
#1122=ORIENTED_EDGE('',*,*,#2126,.T.);
#1123=ORIENTED_EDGE('',*,*,#2127,.T.);
#1124=ORIENTED_EDGE('',*,*,#2128,.T.);
#1125=ORIENTED_EDGE('',*,*,#2129,.T.);
#1126=ORIENTED_EDGE('',*,*,#2130,.T.);
#1127=ORIENTED_EDGE('',*,*,#2131,.T.);
#1128=ORIENTED_EDGE('',*,*,#2132,.T.);
#1129=ORIENTED_EDGE('',*,*,#2133,.T.);
#1130=ORIENTED_EDGE('',*,*,#2134,.T.);
#1131=ORIENTED_EDGE('',*,*,#2135,.T.);
#1132=ORIENTED_EDGE('',*,*,#2136,.T.);
#1133=ORIENTED_EDGE('',*,*,#2049,.T.);
#1134=ORIENTED_EDGE('',*,*,#2137,.T.);
#1135=ORIENTED_EDGE('',*,*,#2138,.T.);
#1136=ORIENTED_EDGE('',*,*,#2139,.T.);
#1137=ORIENTED_EDGE('',*,*,#2140,.T.);
#1138=ORIENTED_EDGE('',*,*,#2141,.T.);
#1139=ORIENTED_EDGE('',*,*,#2142,.F.);
#1140=ORIENTED_EDGE('',*,*,#2143,.T.);
#1141=ORIENTED_EDGE('',*,*,#2144,.T.);
#1142=ORIENTED_EDGE('',*,*,#2108,.F.);
#1143=ORIENTED_EDGE('',*,*,#2145,.T.);
#1144=ORIENTED_EDGE('',*,*,#2098,.T.);
#1145=ORIENTED_EDGE('',*,*,#2146,.T.);
#1146=ORIENTED_EDGE('',*,*,#2047,.F.);
#1147=ORIENTED_EDGE('',*,*,#2147,.T.);
#1148=ORIENTED_EDGE('',*,*,#2148,.T.);
#1149=ORIENTED_EDGE('',*,*,#2149,.T.);
#1150=ORIENTED_EDGE('',*,*,#2150,.T.);
#1151=ORIENTED_EDGE('',*,*,#2151,.T.);
#1152=ORIENTED_EDGE('',*,*,#2152,.T.);
#1153=ORIENTED_EDGE('',*,*,#2153,.T.);
#1154=ORIENTED_EDGE('',*,*,#2154,.T.);
#1155=ORIENTED_EDGE('',*,*,#2152,.F.);
#1156=ORIENTED_EDGE('',*,*,#2155,.T.);
#1157=ORIENTED_EDGE('',*,*,#2112,.T.);
#1158=ORIENTED_EDGE('',*,*,#2156,.T.);
#1159=ORIENTED_EDGE('',*,*,#2102,.F.);
#1160=ORIENTED_EDGE('',*,*,#2157,.T.);
#1161=ORIENTED_EDGE('',*,*,#2142,.T.);
#1162=ORIENTED_EDGE('',*,*,#2158,.T.);
#1163=ORIENTED_EDGE('',*,*,#2159,.T.);
#1164=ORIENTED_EDGE('',*,*,#2160,.T.);
#1165=ORIENTED_EDGE('',*,*,#2161,.T.);
#1166=ORIENTED_EDGE('',*,*,#2162,.T.);
#1167=ORIENTED_EDGE('',*,*,#2163,.F.);
#1168=ORIENTED_EDGE('',*,*,#2164,.T.);
#1169=ORIENTED_EDGE('',*,*,#2165,.T.);
#1170=ORIENTED_EDGE('',*,*,#2166,.T.);
#1171=ORIENTED_EDGE('',*,*,#2161,.F.);
#1172=ORIENTED_EDGE('',*,*,#2167,.T.);
#1173=ORIENTED_EDGE('',*,*,#2168,.T.);
#1174=ORIENTED_EDGE('',*,*,#2169,.T.);
#1175=ORIENTED_EDGE('',*,*,#2170,.T.);
#1176=ORIENTED_EDGE('',*,*,#2171,.T.);
#1177=ORIENTED_EDGE('',*,*,#2172,.T.);
#1178=ORIENTED_EDGE('',*,*,#2173,.T.);
#1179=ORIENTED_EDGE('',*,*,#2168,.F.);
#1180=ORIENTED_EDGE('',*,*,#2174,.T.);
#1181=ORIENTED_EDGE('',*,*,#2163,.T.);
#1182=ORIENTED_EDGE('',*,*,#2175,.T.);
#1183=ORIENTED_EDGE('',*,*,#2176,.T.);
#1184=ORIENTED_EDGE('',*,*,#2177,.T.);
#1185=ORIENTED_EDGE('',*,*,#2172,.F.);
#1186=ORIENTED_EDGE('',*,*,#2178,.T.);
#1187=ORIENTED_EDGE('',*,*,#2179,.T.);
#1188=ORIENTED_EDGE('',*,*,#2180,.T.);
#1189=ORIENTED_EDGE('',*,*,#2181,.T.);
#1190=ORIENTED_EDGE('',*,*,#2182,.T.);
#1191=ORIENTED_EDGE('',*,*,#2183,.T.);
#1192=ORIENTED_EDGE('',*,*,#2184,.T.);
#1193=ORIENTED_EDGE('',*,*,#2185,.F.);
#1194=ORIENTED_EDGE('',*,*,#2186,.T.);
#1195=ORIENTED_EDGE('',*,*,#2187,.T.);
#1196=ORIENTED_EDGE('',*,*,#2188,.T.);
#1197=ORIENTED_EDGE('',*,*,#2189,.T.);
#1198=ORIENTED_EDGE('',*,*,#2190,.T.);
#1199=ORIENTED_EDGE('',*,*,#2183,.F.);
#1200=ORIENTED_EDGE('',*,*,#2191,.T.);
#1201=ORIENTED_EDGE('',*,*,#2192,.T.);
#1202=ORIENTED_EDGE('',*,*,#2193,.T.);
#1203=ORIENTED_EDGE('',*,*,#2187,.F.);
#1204=ORIENTED_EDGE('',*,*,#2194,.T.);
#1205=ORIENTED_EDGE('',*,*,#2195,.T.);
#1206=ORIENTED_EDGE('',*,*,#2196,.T.);
#1207=ORIENTED_EDGE('',*,*,#2192,.F.);
#1208=ORIENTED_EDGE('',*,*,#2197,.T.);
#1209=ORIENTED_EDGE('',*,*,#2185,.T.);
#1210=ORIENTED_EDGE('',*,*,#2198,.T.);
#1211=ORIENTED_EDGE('',*,*,#2199,.T.);
#1212=ORIENTED_EDGE('',*,*,#2200,.T.);
#1213=ORIENTED_EDGE('',*,*,#2201,.T.);
#1214=ORIENTED_EDGE('',*,*,#2202,.T.);
#1215=ORIENTED_EDGE('',*,*,#2203,.T.);
#1216=ORIENTED_EDGE('',*,*,#2204,.T.);
#1217=ORIENTED_EDGE('',*,*,#2205,.F.);
#1218=ORIENTED_EDGE('',*,*,#2206,.T.);
#1219=ORIENTED_EDGE('',*,*,#2207,.T.);
#1220=ORIENTED_EDGE('',*,*,#2085,.F.);
#1221=ORIENTED_EDGE('',*,*,#2208,.T.);
#1222=ORIENTED_EDGE('',*,*,#2209,.F.);
#1223=ORIENTED_EDGE('',*,*,#2210,.T.);
#1224=ORIENTED_EDGE('',*,*,#2205,.T.);
#1225=ORIENTED_EDGE('',*,*,#2211,.T.);
#1226=ORIENTED_EDGE('',*,*,#2212,.T.);
#1227=ORIENTED_EDGE('',*,*,#2213,.T.);
#1228=ORIENTED_EDGE('',*,*,#2209,.T.);
#1229=ORIENTED_EDGE('',*,*,#2214,.T.);
#1230=ORIENTED_EDGE('',*,*,#2135,.F.);
#1231=ORIENTED_EDGE('',*,*,#2215,.F.);
#1232=ORIENTED_EDGE('',*,*,#2216,.T.);
#1233=ORIENTED_EDGE('',*,*,#2217,.T.);
#1234=ORIENTED_EDGE('',*,*,#2077,.F.);
#1235=ORIENTED_EDGE('',*,*,#2218,.T.);
#1236=ORIENTED_EDGE('',*,*,#2219,.F.);
#1237=ORIENTED_EDGE('',*,*,#2220,.T.);
#1238=ORIENTED_EDGE('',*,*,#2215,.T.);
#1239=ORIENTED_EDGE('',*,*,#2221,.T.);
#1240=ORIENTED_EDGE('',*,*,#2222,.T.);
#1241=ORIENTED_EDGE('',*,*,#2223,.T.);
#1242=ORIENTED_EDGE('',*,*,#2219,.T.);
#1243=ORIENTED_EDGE('',*,*,#2224,.T.);
#1244=ORIENTED_EDGE('',*,*,#2127,.F.);
#1245=ORIENTED_EDGE('',*,*,#2225,.T.);
#1246=ORIENTED_EDGE('',*,*,#2226,.T.);
#1247=ORIENTED_EDGE('',*,*,#2227,.T.);
#1248=ORIENTED_EDGE('',*,*,#2131,.F.);
#1249=ORIENTED_EDGE('',*,*,#2228,.T.);
#1250=ORIENTED_EDGE('',*,*,#2089,.F.);
#1251=ORIENTED_EDGE('',*,*,#2229,.T.);
#1252=ORIENTED_EDGE('',*,*,#2230,.T.);
#1253=ORIENTED_EDGE('',*,*,#2231,.T.);
#1254=ORIENTED_EDGE('',*,*,#2123,.F.);
#1255=ORIENTED_EDGE('',*,*,#2232,.T.);
#1256=ORIENTED_EDGE('',*,*,#2081,.F.);
#1257=ORIENTED_EDGE('',*,*,#2233,.F.);
#1258=ORIENTED_EDGE('',*,*,#2178,.F.);
#1259=ORIENTED_EDGE('',*,*,#2234,.F.);
#1260=ORIENTED_EDGE('',*,*,#2182,.F.);
#1261=ORIENTED_EDGE('',*,*,#2234,.T.);
#1262=ORIENTED_EDGE('',*,*,#2174,.F.);
#1263=ORIENTED_EDGE('',*,*,#2235,.F.);
#1264=ORIENTED_EDGE('',*,*,#2179,.F.);
#1265=ORIENTED_EDGE('',*,*,#2233,.T.);
#1266=ORIENTED_EDGE('',*,*,#2181,.F.);
#1267=ORIENTED_EDGE('',*,*,#2236,.F.);
#1268=ORIENTED_EDGE('',*,*,#2164,.F.);
#1269=ORIENTED_EDGE('',*,*,#2235,.T.);
#1270=ORIENTED_EDGE('',*,*,#2167,.F.);
#1271=ORIENTED_EDGE('',*,*,#2236,.T.);
#1272=ORIENTED_EDGE('',*,*,#2180,.F.);
#1273=ORIENTED_EDGE('',*,*,#2237,.T.);
#1274=ORIENTED_EDGE('',*,*,#2238,.T.);
#1275=ORIENTED_EDGE('',*,*,#2239,.T.);
#1276=ORIENTED_EDGE('',*,*,#2240,.F.);
#1277=ORIENTED_EDGE('',*,*,#2241,.F.);
#1278=ORIENTED_EDGE('',*,*,#2130,.F.);
#1279=ORIENTED_EDGE('',*,*,#2242,.F.);
#1280=ORIENTED_EDGE('',*,*,#2190,.F.);
#1281=ORIENTED_EDGE('',*,*,#2242,.T.);
#1282=ORIENTED_EDGE('',*,*,#2129,.F.);
#1283=ORIENTED_EDGE('',*,*,#2243,.F.);
#1284=ORIENTED_EDGE('',*,*,#2184,.F.);
#1285=ORIENTED_EDGE('',*,*,#2241,.T.);
#1286=ORIENTED_EDGE('',*,*,#2189,.F.);
#1287=ORIENTED_EDGE('',*,*,#2244,.F.);
#1288=ORIENTED_EDGE('',*,*,#2228,.F.);
#1289=ORIENTED_EDGE('',*,*,#2243,.T.);
#1290=ORIENTED_EDGE('',*,*,#2136,.F.);
#1291=ORIENTED_EDGE('',*,*,#2245,.F.);
#1292=ORIENTED_EDGE('',*,*,#2198,.F.);
#1293=ORIENTED_EDGE('',*,*,#2244,.T.);
#1294=ORIENTED_EDGE('',*,*,#2188,.F.);
#1295=ORIENTED_EDGE('',*,*,#2246,.F.);
#1296=ORIENTED_EDGE('',*,*,#2090,.F.);
#1297=ORIENTED_EDGE('',*,*,#2214,.F.);
#1298=ORIENTED_EDGE('',*,*,#2247,.F.);
#1299=ORIENTED_EDGE('',*,*,#2199,.F.);
#1300=ORIENTED_EDGE('',*,*,#2245,.T.);
#1301=ORIENTED_EDGE('',*,*,#2246,.T.);
#1302=ORIENTED_EDGE('',*,*,#2193,.F.);
#1303=ORIENTED_EDGE('',*,*,#2248,.F.);
#1304=ORIENTED_EDGE('',*,*,#2083,.F.);
#1305=ORIENTED_EDGE('',*,*,#2247,.T.);
#1306=ORIENTED_EDGE('',*,*,#2211,.F.);
#1307=ORIENTED_EDGE('',*,*,#2249,.F.);
#1308=ORIENTED_EDGE('',*,*,#2200,.F.);
#1309=ORIENTED_EDGE('',*,*,#2248,.T.);
#1310=ORIENTED_EDGE('',*,*,#2196,.F.);
#1311=ORIENTED_EDGE('',*,*,#2250,.F.);
#1312=ORIENTED_EDGE('',*,*,#2084,.F.);
#1313=ORIENTED_EDGE('',*,*,#2249,.T.);
#1314=ORIENTED_EDGE('',*,*,#2208,.F.);
#1315=ORIENTED_EDGE('',*,*,#2250,.T.);
#1316=ORIENTED_EDGE('',*,*,#2195,.F.);
#1317=ORIENTED_EDGE('',*,*,#2137,.F.);
#1318=ORIENTED_EDGE('',*,*,#2251,.T.);
#1319=ORIENTED_EDGE('',*,*,#2024,.F.);
#1320=ORIENTED_EDGE('',*,*,#2252,.T.);
#1321=ORIENTED_EDGE('',*,*,#2227,.F.);
#1322=ORIENTED_EDGE('',*,*,#2253,.T.);
#1323=ORIENTED_EDGE('',*,*,#2144,.F.);
#1324=ORIENTED_EDGE('',*,*,#2254,.F.);
#1325=ORIENTED_EDGE('',*,*,#2254,.T.);
#1326=ORIENTED_EDGE('',*,*,#2143,.F.);
#1327=ORIENTED_EDGE('',*,*,#2255,.F.);
#1328=ORIENTED_EDGE('',*,*,#2132,.F.);
#1329=ORIENTED_EDGE('',*,*,#2255,.T.);
#1330=ORIENTED_EDGE('',*,*,#2157,.F.);
#1331=ORIENTED_EDGE('',*,*,#2256,.F.);
#1332=ORIENTED_EDGE('',*,*,#2133,.F.);
#1333=ORIENTED_EDGE('',*,*,#2256,.T.);
#1334=ORIENTED_EDGE('',*,*,#2101,.F.);
#1335=ORIENTED_EDGE('',*,*,#2257,.F.);
#1336=ORIENTED_EDGE('',*,*,#2134,.F.);
#1337=ORIENTED_EDGE('',*,*,#2100,.F.);
#1338=ORIENTED_EDGE('',*,*,#2258,.T.);
#1339=ORIENTED_EDGE('',*,*,#2212,.F.);
#1340=ORIENTED_EDGE('',*,*,#2257,.T.);
#1341=ORIENTED_EDGE('',*,*,#2149,.F.);
#1342=ORIENTED_EDGE('',*,*,#2259,.T.);
#1343=ORIENTED_EDGE('',*,*,#2026,.F.);
#1344=ORIENTED_EDGE('',*,*,#2260,.T.);
#1345=ORIENTED_EDGE('',*,*,#2150,.F.);
#1346=ORIENTED_EDGE('',*,*,#2261,.T.);
#1347=ORIENTED_EDGE('',*,*,#2225,.F.);
#1348=ORIENTED_EDGE('',*,*,#2262,.F.);
#1349=ORIENTED_EDGE('',*,*,#2262,.T.);
#1350=ORIENTED_EDGE('',*,*,#2088,.F.);
#1351=ORIENTED_EDGE('',*,*,#2263,.F.);
#1352=ORIENTED_EDGE('',*,*,#2151,.F.);
#1353=ORIENTED_EDGE('',*,*,#2263,.T.);
#1354=ORIENTED_EDGE('',*,*,#2087,.F.);
#1355=ORIENTED_EDGE('',*,*,#2264,.F.);
#1356=ORIENTED_EDGE('',*,*,#2155,.F.);
#1357=ORIENTED_EDGE('',*,*,#2264,.T.);
#1358=ORIENTED_EDGE('',*,*,#2086,.F.);
#1359=ORIENTED_EDGE('',*,*,#2265,.F.);
#1360=ORIENTED_EDGE('',*,*,#2113,.F.);
#1361=ORIENTED_EDGE('',*,*,#2207,.F.);
#1362=ORIENTED_EDGE('',*,*,#2266,.T.);
#1363=ORIENTED_EDGE('',*,*,#2106,.F.);
#1364=ORIENTED_EDGE('',*,*,#2265,.T.);
#1365=ORIENTED_EDGE('',*,*,#2267,.F.);
#1366=ORIENTED_EDGE('',*,*,#2122,.F.);
#1367=ORIENTED_EDGE('',*,*,#2268,.F.);
#1368=ORIENTED_EDGE('',*,*,#2177,.F.);
#1369=ORIENTED_EDGE('',*,*,#2268,.T.);
#1370=ORIENTED_EDGE('',*,*,#2121,.F.);
#1371=ORIENTED_EDGE('',*,*,#2269,.F.);
#1372=ORIENTED_EDGE('',*,*,#2173,.F.);
#1373=ORIENTED_EDGE('',*,*,#2267,.T.);
#1374=ORIENTED_EDGE('',*,*,#2176,.F.);
#1375=ORIENTED_EDGE('',*,*,#2270,.F.);
#1376=ORIENTED_EDGE('',*,*,#2232,.F.);
#1377=ORIENTED_EDGE('',*,*,#2269,.T.);
#1378=ORIENTED_EDGE('',*,*,#2128,.F.);
#1379=ORIENTED_EDGE('',*,*,#2271,.F.);
#1380=ORIENTED_EDGE('',*,*,#2169,.F.);
#1381=ORIENTED_EDGE('',*,*,#2270,.T.);
#1382=ORIENTED_EDGE('',*,*,#2175,.F.);
#1383=ORIENTED_EDGE('',*,*,#2272,.F.);
#1384=ORIENTED_EDGE('',*,*,#2082,.F.);
#1385=ORIENTED_EDGE('',*,*,#2224,.F.);
#1386=ORIENTED_EDGE('',*,*,#2273,.F.);
#1387=ORIENTED_EDGE('',*,*,#2170,.F.);
#1388=ORIENTED_EDGE('',*,*,#2271,.T.);
#1389=ORIENTED_EDGE('',*,*,#2272,.T.);
#1390=ORIENTED_EDGE('',*,*,#2162,.F.);
#1391=ORIENTED_EDGE('',*,*,#2274,.F.);
#1392=ORIENTED_EDGE('',*,*,#2075,.F.);
#1393=ORIENTED_EDGE('',*,*,#2273,.T.);
#1394=ORIENTED_EDGE('',*,*,#2221,.F.);
#1395=ORIENTED_EDGE('',*,*,#2275,.F.);
#1396=ORIENTED_EDGE('',*,*,#2171,.F.);
#1397=ORIENTED_EDGE('',*,*,#2274,.T.);
#1398=ORIENTED_EDGE('',*,*,#2166,.F.);
#1399=ORIENTED_EDGE('',*,*,#2276,.F.);
#1400=ORIENTED_EDGE('',*,*,#2076,.F.);
#1401=ORIENTED_EDGE('',*,*,#2275,.T.);
#1402=ORIENTED_EDGE('',*,*,#2218,.F.);
#1403=ORIENTED_EDGE('',*,*,#2276,.T.);
#1404=ORIENTED_EDGE('',*,*,#2165,.F.);
#1405=ORIENTED_EDGE('',*,*,#2147,.F.);
#1406=ORIENTED_EDGE('',*,*,#2277,.T.);
#1407=ORIENTED_EDGE('',*,*,#2029,.F.);
#1408=ORIENTED_EDGE('',*,*,#2278,.T.);
#1409=ORIENTED_EDGE('',*,*,#2231,.F.);
#1410=ORIENTED_EDGE('',*,*,#2279,.T.);
#1411=ORIENTED_EDGE('',*,*,#2154,.F.);
#1412=ORIENTED_EDGE('',*,*,#2280,.F.);
#1413=ORIENTED_EDGE('',*,*,#2280,.T.);
#1414=ORIENTED_EDGE('',*,*,#2153,.F.);
#1415=ORIENTED_EDGE('',*,*,#2281,.F.);
#1416=ORIENTED_EDGE('',*,*,#2124,.F.);
#1417=ORIENTED_EDGE('',*,*,#2281,.T.);
#1418=ORIENTED_EDGE('',*,*,#2156,.F.);
#1419=ORIENTED_EDGE('',*,*,#2282,.F.);
#1420=ORIENTED_EDGE('',*,*,#2125,.F.);
#1421=ORIENTED_EDGE('',*,*,#2282,.T.);
#1422=ORIENTED_EDGE('',*,*,#2111,.F.);
#1423=ORIENTED_EDGE('',*,*,#2283,.F.);
#1424=ORIENTED_EDGE('',*,*,#2126,.F.);
#1425=ORIENTED_EDGE('',*,*,#2110,.F.);
#1426=ORIENTED_EDGE('',*,*,#2284,.T.);
#1427=ORIENTED_EDGE('',*,*,#2222,.F.);
#1428=ORIENTED_EDGE('',*,*,#2283,.T.);
#1429=ORIENTED_EDGE('',*,*,#2031,.F.);
#1430=ORIENTED_EDGE('',*,*,#2285,.T.);
#1431=ORIENTED_EDGE('',*,*,#2139,.F.);
#1432=ORIENTED_EDGE('',*,*,#2286,.T.);
#1433=ORIENTED_EDGE('',*,*,#2140,.F.);
#1434=ORIENTED_EDGE('',*,*,#2287,.T.);
#1435=ORIENTED_EDGE('',*,*,#2229,.F.);
#1436=ORIENTED_EDGE('',*,*,#2288,.F.);
#1437=ORIENTED_EDGE('',*,*,#2288,.T.);
#1438=ORIENTED_EDGE('',*,*,#2080,.F.);
#1439=ORIENTED_EDGE('',*,*,#2289,.F.);
#1440=ORIENTED_EDGE('',*,*,#2141,.F.);
#1441=ORIENTED_EDGE('',*,*,#2289,.T.);
#1442=ORIENTED_EDGE('',*,*,#2079,.F.);
#1443=ORIENTED_EDGE('',*,*,#2290,.F.);
#1444=ORIENTED_EDGE('',*,*,#2158,.F.);
#1445=ORIENTED_EDGE('',*,*,#2290,.T.);
#1446=ORIENTED_EDGE('',*,*,#2078,.F.);
#1447=ORIENTED_EDGE('',*,*,#2291,.F.);
#1448=ORIENTED_EDGE('',*,*,#2103,.F.);
#1449=ORIENTED_EDGE('',*,*,#2217,.F.);
#1450=ORIENTED_EDGE('',*,*,#2292,.T.);
#1451=ORIENTED_EDGE('',*,*,#2104,.F.);
#1452=ORIENTED_EDGE('',*,*,#2291,.T.);
#1453=ORIENTED_EDGE('',*,*,#2293,.F.);
#1454=ORIENTED_EDGE('',*,*,#2204,.F.);
#1455=ORIENTED_EDGE('',*,*,#2294,.F.);
#1456=ORIENTED_EDGE('',*,*,#2197,.F.);
#1457=ORIENTED_EDGE('',*,*,#2294,.T.);
#1458=ORIENTED_EDGE('',*,*,#2203,.F.);
#1459=ORIENTED_EDGE('',*,*,#2295,.F.);
#1460=ORIENTED_EDGE('',*,*,#2186,.F.);
#1461=ORIENTED_EDGE('',*,*,#2293,.T.);
#1462=ORIENTED_EDGE('',*,*,#2194,.F.);
#1463=ORIENTED_EDGE('',*,*,#2296,.F.);
#1464=ORIENTED_EDGE('',*,*,#2201,.F.);
#1465=ORIENTED_EDGE('',*,*,#2295,.T.);
#1466=ORIENTED_EDGE('',*,*,#2202,.F.);
#1467=ORIENTED_EDGE('',*,*,#2296,.T.);
#1468=ORIENTED_EDGE('',*,*,#2191,.F.);
#1469=ORIENTED_EDGE('',*,*,#2297,.F.);
#1470=ORIENTED_EDGE('',*,*,#2287,.F.);
#1471=ORIENTED_EDGE('',*,*,#2285,.F.);
#1472=ORIENTED_EDGE('',*,*,#2298,.F.);
#1473=ORIENTED_EDGE('',*,*,#2230,.F.);
#1474=ORIENTED_EDGE('',*,*,#2297,.T.);
#1475=ORIENTED_EDGE('',*,*,#2030,.F.);
#1476=ORIENTED_EDGE('',*,*,#2298,.T.);
#1477=ORIENTED_EDGE('',*,*,#2277,.F.);
#1478=ORIENTED_EDGE('',*,*,#2279,.F.);
#1479=ORIENTED_EDGE('',*,*,#2299,.F.);
#1480=ORIENTED_EDGE('',*,*,#2252,.F.);
#1481=ORIENTED_EDGE('',*,*,#2064,.F.);
#1482=ORIENTED_EDGE('',*,*,#2299,.T.);
#1483=ORIENTED_EDGE('',*,*,#2042,.F.);
#1484=ORIENTED_EDGE('',*,*,#2300,.F.);
#1485=ORIENTED_EDGE('',*,*,#2138,.F.);
#1486=ORIENTED_EDGE('',*,*,#2286,.F.);
#1487=ORIENTED_EDGE('',*,*,#2300,.T.);
#1488=ORIENTED_EDGE('',*,*,#2066,.F.);
#1489=ORIENTED_EDGE('',*,*,#2068,.T.);
#1490=ORIENTED_EDGE('',*,*,#2259,.F.);
#1491=ORIENTED_EDGE('',*,*,#2301,.F.);
#1492=ORIENTED_EDGE('',*,*,#2301,.T.);
#1493=ORIENTED_EDGE('',*,*,#2148,.F.);
#1494=ORIENTED_EDGE('',*,*,#2302,.F.);
#1495=ORIENTED_EDGE('',*,*,#2037,.F.);
#1496=ORIENTED_EDGE('',*,*,#2302,.T.);
#1497=ORIENTED_EDGE('',*,*,#2278,.F.);
#1498=ORIENTED_EDGE('',*,*,#2070,.T.);
#1499=ORIENTED_EDGE('',*,*,#2303,.F.);
#1500=ORIENTED_EDGE('',*,*,#2261,.F.);
#1501=ORIENTED_EDGE('',*,*,#2260,.F.);
#1502=ORIENTED_EDGE('',*,*,#2304,.F.);
#1503=ORIENTED_EDGE('',*,*,#2226,.F.);
#1504=ORIENTED_EDGE('',*,*,#2303,.T.);
#1505=ORIENTED_EDGE('',*,*,#2025,.F.);
#1506=ORIENTED_EDGE('',*,*,#2304,.T.);
#1507=ORIENTED_EDGE('',*,*,#2251,.F.);
#1508=ORIENTED_EDGE('',*,*,#2253,.F.);
#1509=ORIENTED_EDGE('',*,*,#2305,.F.);
#1510=ORIENTED_EDGE('',*,*,#2145,.F.);
#1511=ORIENTED_EDGE('',*,*,#2306,.F.);
#1512=ORIENTED_EDGE('',*,*,#2096,.F.);
#1513=ORIENTED_EDGE('',*,*,#2306,.T.);
#1514=ORIENTED_EDGE('',*,*,#2107,.F.);
#1515=ORIENTED_EDGE('',*,*,#2307,.F.);
#1516=ORIENTED_EDGE('',*,*,#2091,.F.);
#1517=ORIENTED_EDGE('',*,*,#2305,.T.);
#1518=ORIENTED_EDGE('',*,*,#2095,.F.);
#1519=ORIENTED_EDGE('',*,*,#2308,.F.);
#1520=ORIENTED_EDGE('',*,*,#2099,.F.);
#1521=ORIENTED_EDGE('',*,*,#2307,.T.);
#1522=ORIENTED_EDGE('',*,*,#2266,.F.);
#1523=ORIENTED_EDGE('',*,*,#2309,.F.);
#1524=ORIENTED_EDGE('',*,*,#2258,.F.);
#1525=ORIENTED_EDGE('',*,*,#2308,.T.);
#1526=ORIENTED_EDGE('',*,*,#2310,.F.);
#1527=ORIENTED_EDGE('',*,*,#2309,.T.);
#1528=ORIENTED_EDGE('',*,*,#2206,.F.);
#1529=ORIENTED_EDGE('',*,*,#2311,.F.);
#1530=ORIENTED_EDGE('',*,*,#2092,.F.);
#1531=ORIENTED_EDGE('',*,*,#2310,.T.);
#1532=ORIENTED_EDGE('',*,*,#2094,.F.);
#1533=ORIENTED_EDGE('',*,*,#2312,.F.);
#1534=ORIENTED_EDGE('',*,*,#2213,.F.);
#1535=ORIENTED_EDGE('',*,*,#2311,.T.);
#1536=ORIENTED_EDGE('',*,*,#2210,.F.);
#1537=ORIENTED_EDGE('',*,*,#2312,.T.);
#1538=ORIENTED_EDGE('',*,*,#2093,.F.);
#1539=ORIENTED_EDGE('',*,*,#2097,.F.);
#1540=ORIENTED_EDGE('',*,*,#2240,.T.);
#1541=ORIENTED_EDGE('',*,*,#2159,.F.);
#1542=ORIENTED_EDGE('',*,*,#2239,.F.);
#1543=ORIENTED_EDGE('',*,*,#2237,.F.);
#1544=ORIENTED_EDGE('',*,*,#2160,.F.);
#1545=ORIENTED_EDGE('',*,*,#2313,.F.);
#1546=ORIENTED_EDGE('',*,*,#2119,.F.);
#1547=ORIENTED_EDGE('',*,*,#2314,.F.);
#1548=ORIENTED_EDGE('',*,*,#2146,.F.);
#1549=ORIENTED_EDGE('',*,*,#2314,.T.);
#1550=ORIENTED_EDGE('',*,*,#2118,.F.);
#1551=ORIENTED_EDGE('',*,*,#2315,.F.);
#1552=ORIENTED_EDGE('',*,*,#2109,.F.);
#1553=ORIENTED_EDGE('',*,*,#2313,.T.);
#1554=ORIENTED_EDGE('',*,*,#2105,.F.);
#1555=ORIENTED_EDGE('',*,*,#2316,.F.);
#1556=ORIENTED_EDGE('',*,*,#2114,.F.);
#1557=ORIENTED_EDGE('',*,*,#2284,.F.);
#1558=ORIENTED_EDGE('',*,*,#2315,.T.);
#1559=ORIENTED_EDGE('',*,*,#2317,.F.);
#1560=ORIENTED_EDGE('',*,*,#2316,.T.);
#1561=ORIENTED_EDGE('',*,*,#2292,.F.);
#1562=ORIENTED_EDGE('',*,*,#2318,.F.);
#1563=ORIENTED_EDGE('',*,*,#2317,.T.);
#1564=ORIENTED_EDGE('',*,*,#2117,.F.);
#1565=ORIENTED_EDGE('',*,*,#2319,.F.);
#1566=ORIENTED_EDGE('',*,*,#2223,.F.);
#1567=ORIENTED_EDGE('',*,*,#2318,.T.);
#1568=ORIENTED_EDGE('',*,*,#2216,.F.);
#1569=ORIENTED_EDGE('',*,*,#2320,.F.);
#1570=ORIENTED_EDGE('',*,*,#2115,.F.);
#1571=ORIENTED_EDGE('',*,*,#2319,.T.);
#1572=ORIENTED_EDGE('',*,*,#2116,.F.);
#1573=ORIENTED_EDGE('',*,*,#2320,.T.);
#1574=ORIENTED_EDGE('',*,*,#2220,.F.);
#1575=ORIENTED_EDGE('',*,*,#2120,.F.);
#1576=ORIENTED_EDGE('',*,*,#2238,.F.);
#1577=ORIENTED_EDGE('',*,*,#2027,.T.);
#1578=ORIENTED_EDGE('',*,*,#2072,.T.);
#1579=ORIENTED_EDGE('',*,*,#2053,.T.);
#1580=ORIENTED_EDGE('',*,*,#2056,.F.);
#1581=ORIENTED_EDGE('',*,*,#2043,.T.);
#1582=ORIENTED_EDGE('',*,*,#2061,.F.);
#1583=ORIENTED_EDGE('',*,*,#2058,.F.);
#1584=ORIENTED_EDGE('',*,*,#2074,.T.);
#1585=ORIENTED_EDGE('',*,*,#2020,.F.);
#1586=ORIENTED_EDGE('',*,*,#2067,.F.);
#1587=ORIENTED_EDGE('',*,*,#2035,.T.);
#1588=ORIENTED_EDGE('',*,*,#2069,.F.);
#1589=ORIENTED_EDGE('',*,*,#2048,.T.);
#1590=ORIENTED_EDGE('',*,*,#2051,.T.);
#1591=ORIENTED_EDGE('',*,*,#2071,.T.);
#1592=ORIENTED_EDGE('',*,*,#2033,.T.);
#1593=ORIENTED_EDGE('',*,*,#2065,.F.);
#1594=ORIENTED_EDGE('',*,*,#2040,.F.);
#1595=ORIENTED_EDGE('',*,*,#2063,.F.);
#1596=ORIENTED_EDGE('',*,*,#2022,.F.);
#1597=ORIENTED_EDGE('',*,*,#2073,.T.);
#1598=ORIENTED_EDGE('',*,*,#2060,.F.);
#1599=ORIENTED_EDGE('',*,*,#2062,.F.);
#1600=ORIENTED_EDGE('',*,*,#2045,.T.);
#1601=ORIENTED_EDGE('',*,*,#2055,.F.);
#1602=ORIENTED_EDGE('',*,*,#2050,.T.);
#2019=EDGE_CURVE('',#2564,#2565,#2890,.T.);
#2020=EDGE_CURVE('',#2565,#2566,#2891,.T.);
#2021=EDGE_CURVE('',#2566,#2567,#374,.F.);
#2022=EDGE_CURVE('',#2567,#2568,#2892,.T.);
#2023=EDGE_CURVE('',#2568,#2569,#2893,.F.);
#2024=EDGE_CURVE('',#2569,#2570,#375,.F.);
#2025=EDGE_CURVE('',#2570,#2571,#376,.T.);
#2026=EDGE_CURVE('',#2571,#2564,#377,.F.);
#2027=EDGE_CURVE('',#2572,#2573,#2894,.T.);
#2028=EDGE_CURVE('',#2572,#2574,#2895,.F.);
#2029=EDGE_CURVE('',#2574,#2575,#378,.T.);
#2030=EDGE_CURVE('',#2575,#2576,#379,.F.);
#2031=EDGE_CURVE('',#2576,#2577,#380,.T.);
#2032=EDGE_CURVE('',#2577,#2578,#2896,.T.);
#2033=EDGE_CURVE('',#2579,#2578,#2897,.T.);
#2034=EDGE_CURVE('',#2579,#2573,#381,.T.);
#2035=EDGE_CURVE('',#2580,#2581,#2898,.T.);
#2036=EDGE_CURVE('',#2580,#2582,#2899,.F.);
#2037=EDGE_CURVE('',#2582,#2583,#2900,.F.);
#2038=EDGE_CURVE('',#2583,#2581,#2901,.T.);
#2039=EDGE_CURVE('',#2584,#2585,#2902,.T.);
#2040=EDGE_CURVE('',#2585,#2586,#2903,.T.);
#2041=EDGE_CURVE('',#2586,#2587,#2904,.F.);
#2042=EDGE_CURVE('',#2587,#2584,#2905,.T.);
#2043=EDGE_CURVE('',#2588,#2589,#2906,.F.);
#2044=EDGE_CURVE('',#2588,#2590,#382,.T.);
#2045=EDGE_CURVE('',#2591,#2590,#2907,.T.);
#2046=EDGE_CURVE('',#2589,#2591,#383,.T.);
#2047=EDGE_CURVE('',#2592,#2592,#607,.T.);
#2048=EDGE_CURVE('',#2593,#2593,#384,.F.);
#2049=EDGE_CURVE('',#2594,#2594,#608,.T.);
#2050=EDGE_CURVE('',#2595,#2595,#385,.F.);
#2051=EDGE_CURVE('',#2596,#2597,#2908,.T.);
#2052=EDGE_CURVE('',#2598,#2596,#386,.T.);
#2053=EDGE_CURVE('',#2599,#2598,#2909,.F.);
#2054=EDGE_CURVE('',#2599,#2597,#387,.F.);
#2055=EDGE_CURVE('',#2596,#2590,#2910,.T.);
#2056=EDGE_CURVE('',#2588,#2598,#2911,.T.);
#2057=EDGE_CURVE('',#2600,#2601,#388,.T.);
#2058=EDGE_CURVE('',#2601,#2602,#2912,.F.);
#2059=EDGE_CURVE('',#2602,#2603,#389,.T.);
#2060=EDGE_CURVE('',#2603,#2600,#2913,.T.);
#2061=EDGE_CURVE('',#2602,#2589,#2914,.T.);
#2062=EDGE_CURVE('',#2591,#2603,#2915,.T.);
#2063=EDGE_CURVE('',#2568,#2585,#390,.F.);
#2064=EDGE_CURVE('',#2584,#2569,#391,.T.);
#2065=EDGE_CURVE('',#2586,#2578,#392,.F.);
#2066=EDGE_CURVE('',#2577,#2587,#393,.T.);
#2067=EDGE_CURVE('',#2580,#2565,#394,.F.);
#2068=EDGE_CURVE('',#2582,#2564,#395,.T.);
#2069=EDGE_CURVE('',#2572,#2581,#396,.F.);
#2070=EDGE_CURVE('',#2574,#2583,#397,.T.);
#2071=EDGE_CURVE('',#2597,#2579,#609,.T.);
#2072=EDGE_CURVE('',#2573,#2599,#610,.T.);
#2073=EDGE_CURVE('',#2567,#2600,#611,.T.);
#2074=EDGE_CURVE('',#2601,#2566,#612,.T.);
#2075=EDGE_CURVE('',#2604,#2605,#2916,.F.);
#2076=EDGE_CURVE('',#2605,#2606,#398,.T.);
#2077=EDGE_CURVE('',#2606,#2607,#399,.T.);
#2078=EDGE_CURVE('',#2607,#2608,#400,.T.);
#2079=EDGE_CURVE('',#2608,#2609,#2917,.F.);
#2080=EDGE_CURVE('',#2609,#2610,#401,.T.);
#2081=EDGE_CURVE('',#2610,#2611,#402,.T.);
#2082=EDGE_CURVE('',#2611,#2604,#403,.T.);
#2083=EDGE_CURVE('',#2612,#2613,#2918,.F.);
#2084=EDGE_CURVE('',#2613,#2614,#404,.F.);
#2085=EDGE_CURVE('',#2614,#2615,#405,.F.);
#2086=EDGE_CURVE('',#2615,#2616,#406,.F.);
#2087=EDGE_CURVE('',#2616,#2617,#2919,.F.);
#2088=EDGE_CURVE('',#2617,#2618,#407,.F.);
#2089=EDGE_CURVE('',#2618,#2619,#408,.F.);
#2090=EDGE_CURVE('',#2619,#2612,#409,.F.);
#2091=EDGE_CURVE('',#2620,#2621,#410,.F.);
#2092=EDGE_CURVE('',#2621,#2622,#411,.T.);
#2093=EDGE_CURVE('',#2622,#2623,#2920,.T.);
#2094=EDGE_CURVE('',#2623,#2624,#412,.T.);
#2095=EDGE_CURVE('',#2624,#2625,#413,.F.);
#2096=EDGE_CURVE('',#2625,#2620,#414,.T.);
#2097=EDGE_CURVE('',#2626,#2626,#415,.F.);
#2098=EDGE_CURVE('',#2627,#2628,#2921,.T.);
#2099=EDGE_CURVE('',#2627,#2629,#416,.T.);
#2100=EDGE_CURVE('',#2629,#2630,#613,.T.);
#2101=EDGE_CURVE('',#2630,#2631,#417,.T.);
#2102=EDGE_CURVE('',#2631,#2632,#2922,.T.);
#2103=EDGE_CURVE('',#2632,#2633,#418,.F.);
#2104=EDGE_CURVE('',#2633,#2634,#614,.T.);
#2105=EDGE_CURVE('',#2634,#2628,#419,.F.);
#2106=EDGE_CURVE('',#2635,#2636,#615,.T.);
#2107=EDGE_CURVE('',#2636,#2637,#420,.T.);
#2108=EDGE_CURVE('',#2637,#2638,#2923,.T.);
#2109=EDGE_CURVE('',#2638,#2639,#421,.F.);
#2110=EDGE_CURVE('',#2639,#2640,#616,.T.);
#2111=EDGE_CURVE('',#2640,#2641,#422,.F.);
#2112=EDGE_CURVE('',#2642,#2641,#2924,.T.);
#2113=EDGE_CURVE('',#2642,#2635,#423,.T.);
#2114=EDGE_CURVE('',#2643,#2644,#424,.T.);
#2115=EDGE_CURVE('',#2644,#2645,#425,.F.);
#2116=EDGE_CURVE('',#2645,#2646,#2925,.F.);
#2117=EDGE_CURVE('',#2646,#2647,#426,.F.);
#2118=EDGE_CURVE('',#2647,#2648,#427,.T.);
#2119=EDGE_CURVE('',#2648,#2643,#428,.F.);
#2120=EDGE_CURVE('',#2649,#2649,#429,.T.);
#2121=EDGE_CURVE('',#2650,#2651,#2926,.T.);
#2122=EDGE_CURVE('',#2651,#2652,#430,.T.);
#2123=EDGE_CURVE('',#2652,#2653,#431,.T.);
#2124=EDGE_CURVE('',#2653,#2654,#432,.T.);
#2125=EDGE_CURVE('',#2654,#2655,#2927,.T.);
#2126=EDGE_CURVE('',#2655,#2656,#433,.T.);
#2127=EDGE_CURVE('',#2656,#2657,#434,.T.);
#2128=EDGE_CURVE('',#2657,#2650,#435,.T.);
#2129=EDGE_CURVE('',#2658,#2659,#2928,.T.);
#2130=EDGE_CURVE('',#2659,#2660,#436,.F.);
#2131=EDGE_CURVE('',#2660,#2661,#437,.F.);
#2132=EDGE_CURVE('',#2661,#2662,#438,.F.);
#2133=EDGE_CURVE('',#2662,#2663,#2929,.T.);
#2134=EDGE_CURVE('',#2663,#2664,#439,.F.);
#2135=EDGE_CURVE('',#2664,#2665,#440,.F.);
#2136=EDGE_CURVE('',#2665,#2658,#441,.F.);
#2137=EDGE_CURVE('',#2666,#2667,#442,.T.);
#2138=EDGE_CURVE('',#2667,#2668,#2930,.T.);
#2139=EDGE_CURVE('',#2668,#2669,#443,.F.);
#2140=EDGE_CURVE('',#2669,#2670,#617,.T.);
#2141=EDGE_CURVE('',#2670,#2671,#444,.F.);
#2142=EDGE_CURVE('',#2672,#2671,#2931,.T.);
#2143=EDGE_CURVE('',#2672,#2673,#445,.T.);
#2144=EDGE_CURVE('',#2673,#2666,#618,.T.);
#2145=EDGE_CURVE('',#2637,#2627,#446,.F.);
#2146=EDGE_CURVE('',#2628,#2638,#447,.T.);
#2147=EDGE_CURVE('',#2674,#2675,#448,.F.);
#2148=EDGE_CURVE('',#2675,#2676,#2932,.F.);
#2149=EDGE_CURVE('',#2676,#2677,#449,.T.);
#2150=EDGE_CURVE('',#2677,#2678,#619,.T.);
#2151=EDGE_CURVE('',#2678,#2679,#450,.T.);
#2152=EDGE_CURVE('',#2679,#2680,#2933,.T.);
#2153=EDGE_CURVE('',#2680,#2681,#451,.F.);
#2154=EDGE_CURVE('',#2681,#2674,#620,.T.);
#2155=EDGE_CURVE('',#2679,#2642,#2934,.T.);
#2156=EDGE_CURVE('',#2641,#2680,#2935,.F.);
#2157=EDGE_CURVE('',#2631,#2672,#2936,.F.);
#2158=EDGE_CURVE('',#2671,#2632,#2937,.T.);
#2159=EDGE_CURVE('',#2682,#2682,#452,.T.);
#2160=EDGE_CURVE('',#2683,#2683,#453,.T.);
#2161=EDGE_CURVE('',#2684,#2685,#2938,.T.);
#2162=EDGE_CURVE('',#2685,#2686,#2939,.T.);
#2163=EDGE_CURVE('',#2687,#2686,#2940,.T.);
#2164=EDGE_CURVE('',#2687,#2684,#2941,.F.);
#2165=EDGE_CURVE('',#2688,#2689,#621,.T.);
#2166=EDGE_CURVE('',#2689,#2685,#454,.F.);
#2167=EDGE_CURVE('',#2684,#2690,#455,.F.);
#2168=EDGE_CURVE('',#2690,#2691,#2942,.T.);
#2169=EDGE_CURVE('',#2691,#2692,#456,.F.);
#2170=EDGE_CURVE('',#2692,#2693,#622,.T.);
#2171=EDGE_CURVE('',#2693,#2688,#623,.T.);
#2172=EDGE_CURVE('',#2694,#2695,#2943,.T.);
#2173=EDGE_CURVE('',#2695,#2691,#2944,.F.);
#2174=EDGE_CURVE('',#2690,#2694,#2945,.T.);
#2175=EDGE_CURVE('',#2686,#2696,#457,.F.);
#2176=EDGE_CURVE('',#2696,#2697,#624,.T.);
#2177=EDGE_CURVE('',#2697,#2695,#458,.F.);
#2178=EDGE_CURVE('',#2694,#2687,#459,.F.);
#2179=EDGE_CURVE('',#2698,#2699,#2946,.F.);
#2180=EDGE_CURVE('',#2699,#2700,#460,.T.);
#2181=EDGE_CURVE('',#2700,#2701,#2947,.T.);
#2182=EDGE_CURVE('',#2701,#2698,#461,.T.);
#2183=EDGE_CURVE('',#2702,#2703,#2948,.T.);
#2184=EDGE_CURVE('',#2703,#2704,#2949,.F.);
#2185=EDGE_CURVE('',#2705,#2704,#2950,.T.);
#2186=EDGE_CURVE('',#2705,#2702,#2951,.T.);
#2187=EDGE_CURVE('',#2706,#2707,#2952,.T.);
#2188=EDGE_CURVE('',#2707,#2708,#462,.T.);
#2189=EDGE_CURVE('',#2708,#2709,#625,.T.);
#2190=EDGE_CURVE('',#2709,#2703,#463,.T.);
#2191=EDGE_CURVE('',#2702,#2706,#464,.F.);
#2192=EDGE_CURVE('',#2710,#2711,#2953,.T.);
#2193=EDGE_CURVE('',#2711,#2707,#2954,.T.);
#2194=EDGE_CURVE('',#2706,#2710,#2955,.F.);
#2195=EDGE_CURVE('',#2712,#2713,#626,.T.);
#2196=EDGE_CURVE('',#2713,#2711,#465,.T.);
#2197=EDGE_CURVE('',#2710,#2705,#466,.F.);
#2198=EDGE_CURVE('',#2704,#2714,#467,.T.);
#2199=EDGE_CURVE('',#2714,#2715,#627,.T.);
#2200=EDGE_CURVE('',#2715,#2712,#628,.T.);
#2201=EDGE_CURVE('',#2716,#2717,#2956,.T.);
#2202=EDGE_CURVE('',#2717,#2718,#468,.T.);
#2203=EDGE_CURVE('',#2718,#2719,#2957,.F.);
#2204=EDGE_CURVE('',#2719,#2716,#469,.T.);
#2205=EDGE_CURVE('',#2720,#2721,#629,.T.);
#2206=EDGE_CURVE('',#2720,#2722,#470,.F.);
#2207=EDGE_CURVE('',#2722,#2615,#630,.T.);
#2208=EDGE_CURVE('',#2614,#2721,#631,.T.);
#2209=EDGE_CURVE('',#2723,#2724,#632,.T.);
#2210=EDGE_CURVE('',#2723,#2720,#2958,.T.);
#2211=EDGE_CURVE('',#2721,#2724,#633,.T.);
#2212=EDGE_CURVE('',#2664,#2725,#634,.T.);
#2213=EDGE_CURVE('',#2725,#2723,#471,.F.);
#2214=EDGE_CURVE('',#2724,#2665,#635,.T.);
#2215=EDGE_CURVE('',#2726,#2727,#636,.T.);
#2216=EDGE_CURVE('',#2726,#2728,#472,.F.);
#2217=EDGE_CURVE('',#2728,#2607,#637,.T.);
#2218=EDGE_CURVE('',#2606,#2727,#638,.T.);
#2219=EDGE_CURVE('',#2729,#2730,#639,.T.);
#2220=EDGE_CURVE('',#2729,#2726,#2959,.T.);
#2221=EDGE_CURVE('',#2727,#2730,#640,.T.);
#2222=EDGE_CURVE('',#2656,#2731,#641,.T.);
#2223=EDGE_CURVE('',#2731,#2729,#473,.F.);
#2224=EDGE_CURVE('',#2730,#2657,#642,.T.);
#2225=EDGE_CURVE('',#2618,#2732,#643,.T.);
#2226=EDGE_CURVE('',#2732,#2733,#474,.F.);
#2227=EDGE_CURVE('',#2733,#2661,#644,.T.);
#2228=EDGE_CURVE('',#2660,#2619,#645,.T.);
#2229=EDGE_CURVE('',#2610,#2734,#646,.T.);
#2230=EDGE_CURVE('',#2734,#2735,#475,.F.);
#2231=EDGE_CURVE('',#2735,#2653,#647,.T.);
#2232=EDGE_CURVE('',#2652,#2611,#648,.T.);
#2233=EDGE_CURVE('',#2687,#2701,#649,.T.);
#2234=EDGE_CURVE('',#2698,#2694,#650,.F.);
#2235=EDGE_CURVE('',#2699,#2690,#651,.F.);
#2236=EDGE_CURVE('',#2684,#2700,#652,.T.);
#2237=EDGE_CURVE('',#2736,#2736,#476,.F.);
#2238=EDGE_CURVE('',#2737,#2737,#477,.T.);
#2239=EDGE_CURVE('',#2738,#2738,#478,.F.);
#2240=EDGE_CURVE('',#2739,#2739,#479,.T.);
#2241=EDGE_CURVE('',#2660,#2709,#480,.T.);
#2242=EDGE_CURVE('',#2703,#2659,#653,.T.);
#2243=EDGE_CURVE('',#2704,#2658,#654,.T.);
#2244=EDGE_CURVE('',#2619,#2708,#481,.T.);
#2245=EDGE_CURVE('',#2714,#2665,#482,.T.);
#2246=EDGE_CURVE('',#2612,#2707,#655,.F.);
#2247=EDGE_CURVE('',#2715,#2724,#656,.T.);
#2248=EDGE_CURVE('',#2613,#2711,#657,.F.);
#2249=EDGE_CURVE('',#2712,#2721,#658,.F.);
#2250=EDGE_CURVE('',#2614,#2713,#483,.T.);
#2251=EDGE_CURVE('',#2666,#2570,#484,.T.);
#2252=EDGE_CURVE('',#2569,#2667,#485,.F.);
#2253=EDGE_CURVE('',#2733,#2666,#486,.F.);
#2254=EDGE_CURVE('',#2661,#2673,#487,.T.);
#2255=EDGE_CURVE('',#2662,#2672,#488,.T.);
#2256=EDGE_CURVE('',#2663,#2631,#489,.T.);
#2257=EDGE_CURVE('',#2664,#2630,#490,.T.);
#2258=EDGE_CURVE('',#2629,#2725,#491,.T.);
#2259=EDGE_CURVE('',#2676,#2564,#492,.T.);
#2260=EDGE_CURVE('',#2571,#2677,#493,.F.);
#2261=EDGE_CURVE('',#2677,#2732,#494,.T.);
#2262=EDGE_CURVE('',#2678,#2618,#495,.T.);
#2263=EDGE_CURVE('',#2679,#2617,#496,.T.);
#2264=EDGE_CURVE('',#2642,#2616,#497,.T.);
#2265=EDGE_CURVE('',#2635,#2615,#498,.T.);
#2266=EDGE_CURVE('',#2722,#2636,#499,.F.);
#2267=EDGE_CURVE('',#2652,#2697,#500,.T.);
#2268=EDGE_CURVE('',#2695,#2651,#659,.T.);
#2269=EDGE_CURVE('',#2691,#2650,#660,.T.);
#2270=EDGE_CURVE('',#2611,#2696,#501,.T.);
#2271=EDGE_CURVE('',#2692,#2657,#502,.T.);
#2272=EDGE_CURVE('',#2604,#2686,#661,.F.);
#2273=EDGE_CURVE('',#2693,#2730,#662,.T.);
#2274=EDGE_CURVE('',#2605,#2685,#663,.F.);
#2275=EDGE_CURVE('',#2688,#2727,#664,.F.);
#2276=EDGE_CURVE('',#2606,#2689,#503,.T.);
#2277=EDGE_CURVE('',#2674,#2575,#504,.F.);
#2278=EDGE_CURVE('',#2574,#2675,#505,.T.);
#2279=EDGE_CURVE('',#2735,#2674,#506,.F.);
#2280=EDGE_CURVE('',#2653,#2681,#507,.T.);
#2281=EDGE_CURVE('',#2654,#2680,#508,.T.);
#2282=EDGE_CURVE('',#2655,#2641,#509,.T.);
#2283=EDGE_CURVE('',#2656,#2640,#510,.T.);
#2284=EDGE_CURVE('',#2639,#2731,#511,.T.);
#2285=EDGE_CURVE('',#2576,#2669,#512,.T.);
#2286=EDGE_CURVE('',#2668,#2577,#513,.F.);
#2287=EDGE_CURVE('',#2669,#2734,#514,.T.);
#2288=EDGE_CURVE('',#2670,#2610,#515,.T.);
#2289=EDGE_CURVE('',#2671,#2609,#516,.T.);
#2290=EDGE_CURVE('',#2632,#2608,#517,.T.);
#2291=EDGE_CURVE('',#2633,#2607,#518,.T.);
#2292=EDGE_CURVE('',#2728,#2634,#519,.F.);
#2293=EDGE_CURVE('',#2716,#2710,#665,.F.);
#2294=EDGE_CURVE('',#2705,#2719,#666,.T.);
#2295=EDGE_CURVE('',#2702,#2718,#667,.T.);
#2296=EDGE_CURVE('',#2717,#2706,#668,.F.);
#2297=EDGE_CURVE('',#2734,#2576,#520,.T.);
#2298=EDGE_CURVE('',#2735,#2575,#521,.T.);
#2299=EDGE_CURVE('',#2667,#2584,#522,.T.);
#2300=EDGE_CURVE('',#2668,#2587,#523,.T.);
#2301=EDGE_CURVE('',#2582,#2676,#524,.T.);
#2302=EDGE_CURVE('',#2583,#2675,#525,.T.);
#2303=EDGE_CURVE('',#2732,#2571,#526,.T.);
#2304=EDGE_CURVE('',#2733,#2570,#527,.T.);
#2305=EDGE_CURVE('',#2627,#2625,#528,.T.);
#2306=EDGE_CURVE('',#2620,#2637,#529,.T.);
#2307=EDGE_CURVE('',#2621,#2636,#530,.T.);
#2308=EDGE_CURVE('',#2629,#2624,#531,.T.);
#2309=EDGE_CURVE('',#2621,#2722,#532,.T.);
#2310=EDGE_CURVE('',#2725,#2624,#533,.T.);
#2311=EDGE_CURVE('',#2622,#2720,#669,.F.);
#2312=EDGE_CURVE('',#2723,#2623,#670,.T.);
#2313=EDGE_CURVE('',#2643,#2628,#534,.T.);
#2314=EDGE_CURVE('',#2638,#2648,#535,.T.);
#2315=EDGE_CURVE('',#2639,#2647,#536,.T.);
#2316=EDGE_CURVE('',#2644,#2634,#537,.T.);
#2317=EDGE_CURVE('',#2731,#2647,#538,.T.);
#2318=EDGE_CURVE('',#2644,#2728,#539,.T.);
#2319=EDGE_CURVE('',#2729,#2646,#671,.T.);
#2320=EDGE_CURVE('',#2645,#2726,#672,.F.);
#2564=VERTEX_POINT('',#6905);
#2565=VERTEX_POINT('',#6906);
#2566=VERTEX_POINT('',#6908);
#2567=VERTEX_POINT('',#6910);
#2568=VERTEX_POINT('',#6912);
#2569=VERTEX_POINT('',#6914);
#2570=VERTEX_POINT('',#6916);
#2571=VERTEX_POINT('',#6918);
#2572=VERTEX_POINT('',#6922);
#2573=VERTEX_POINT('',#6923);
#2574=VERTEX_POINT('',#6925);
#2575=VERTEX_POINT('',#6927);
#2576=VERTEX_POINT('',#6929);
#2577=VERTEX_POINT('',#6931);
#2578=VERTEX_POINT('',#6933);
#2579=VERTEX_POINT('',#6935);
#2580=VERTEX_POINT('',#6939);
#2581=VERTEX_POINT('',#6940);
#2582=VERTEX_POINT('',#6942);
#2583=VERTEX_POINT('',#6944);
#2584=VERTEX_POINT('',#6948);
#2585=VERTEX_POINT('',#6949);
#2586=VERTEX_POINT('',#6951);
#2587=VERTEX_POINT('',#6953);
#2588=VERTEX_POINT('',#6957);
#2589=VERTEX_POINT('',#6958);
#2590=VERTEX_POINT('',#6960);
#2591=VERTEX_POINT('',#6962);
#2592=VERTEX_POINT('',#6984);
#2593=VERTEX_POINT('',#6986);
#2594=VERTEX_POINT('',#7007);
#2595=VERTEX_POINT('',#7009);
#2596=VERTEX_POINT('',#7012);
#2597=VERTEX_POINT('',#7013);
#2598=VERTEX_POINT('',#7015);
#2599=VERTEX_POINT('',#7017);
#2600=VERTEX_POINT('',#7024);
#2601=VERTEX_POINT('',#7025);
#2602=VERTEX_POINT('',#7027);
#2603=VERTEX_POINT('',#7029);
#2604=VERTEX_POINT('',#7070);
#2605=VERTEX_POINT('',#7071);
#2606=VERTEX_POINT('',#7073);
#2607=VERTEX_POINT('',#7075);
#2608=VERTEX_POINT('',#7077);
#2609=VERTEX_POINT('',#7079);
#2610=VERTEX_POINT('',#7081);
#2611=VERTEX_POINT('',#7083);
#2612=VERTEX_POINT('',#7087);
#2613=VERTEX_POINT('',#7088);
#2614=VERTEX_POINT('',#7090);
#2615=VERTEX_POINT('',#7092);
#2616=VERTEX_POINT('',#7094);
#2617=VERTEX_POINT('',#7096);
#2618=VERTEX_POINT('',#7098);
#2619=VERTEX_POINT('',#7100);
#2620=VERTEX_POINT('',#7104);
#2621=VERTEX_POINT('',#7105);
#2622=VERTEX_POINT('',#7107);
#2623=VERTEX_POINT('',#7109);
#2624=VERTEX_POINT('',#7111);
#2625=VERTEX_POINT('',#7113);
#2626=VERTEX_POINT('',#7116);
#2627=VERTEX_POINT('',#7119);
#2628=VERTEX_POINT('',#7120);
#2629=VERTEX_POINT('',#7122);
#2630=VERTEX_POINT('',#7130);
#2631=VERTEX_POINT('',#7132);
#2632=VERTEX_POINT('',#7134);
#2633=VERTEX_POINT('',#7136);
#2634=VERTEX_POINT('',#7144);
#2635=VERTEX_POINT('',#7154);
#2636=VERTEX_POINT('',#7155);
#2637=VERTEX_POINT('',#7157);
#2638=VERTEX_POINT('',#7159);
#2639=VERTEX_POINT('',#7161);
#2640=VERTEX_POINT('',#7169);
#2641=VERTEX_POINT('',#7171);
#2642=VERTEX_POINT('',#7173);
#2643=VERTEX_POINT('',#7177);
#2644=VERTEX_POINT('',#7178);
#2645=VERTEX_POINT('',#7180);
#2646=VERTEX_POINT('',#7182);
#2647=VERTEX_POINT('',#7184);
#2648=VERTEX_POINT('',#7186);
#2649=VERTEX_POINT('',#7189);
#2650=VERTEX_POINT('',#7192);
#2651=VERTEX_POINT('',#7193);
#2652=VERTEX_POINT('',#7195);
#2653=VERTEX_POINT('',#7197);
#2654=VERTEX_POINT('',#7199);
#2655=VERTEX_POINT('',#7201);
#2656=VERTEX_POINT('',#7203);
#2657=VERTEX_POINT('',#7205);
#2658=VERTEX_POINT('',#7209);
#2659=VERTEX_POINT('',#7210);
#2660=VERTEX_POINT('',#7212);
#2661=VERTEX_POINT('',#7214);
#2662=VERTEX_POINT('',#7216);
#2663=VERTEX_POINT('',#7218);
#2664=VERTEX_POINT('',#7220);
#2665=VERTEX_POINT('',#7222);
#2666=VERTEX_POINT('',#7226);
#2667=VERTEX_POINT('',#7227);
#2668=VERTEX_POINT('',#7229);
#2669=VERTEX_POINT('',#7231);
#2670=VERTEX_POINT('',#7237);
#2671=VERTEX_POINT('',#7239);
#2672=VERTEX_POINT('',#7241);
#2673=VERTEX_POINT('',#7243);
#2674=VERTEX_POINT('',#7254);
#2675=VERTEX_POINT('',#7255);
#2676=VERTEX_POINT('',#7257);
#2677=VERTEX_POINT('',#7259);
#2678=VERTEX_POINT('',#7265);
#2679=VERTEX_POINT('',#7267);
#2680=VERTEX_POINT('',#7269);
#2681=VERTEX_POINT('',#7271);
#2682=VERTEX_POINT('',#7285);
#2683=VERTEX_POINT('',#7287);
#2684=VERTEX_POINT('',#7290);
#2685=VERTEX_POINT('',#7291);
#2686=VERTEX_POINT('',#7293);
#2687=VERTEX_POINT('',#7295);
#2688=VERTEX_POINT('',#7302);
#2689=VERTEX_POINT('',#7303);
#2690=VERTEX_POINT('',#7306);
#2691=VERTEX_POINT('',#7308);
#2692=VERTEX_POINT('',#7310);
#2693=VERTEX_POINT('',#7315);
#2694=VERTEX_POINT('',#7322);
#2695=VERTEX_POINT('',#7323);
#2696=VERTEX_POINT('',#7328);
#2697=VERTEX_POINT('',#7333);
#2698=VERTEX_POINT('',#7338);
#2699=VERTEX_POINT('',#7339);
#2700=VERTEX_POINT('',#7341);
#2701=VERTEX_POINT('',#7343);
#2702=VERTEX_POINT('',#7347);
#2703=VERTEX_POINT('',#7348);
#2704=VERTEX_POINT('',#7350);
#2705=VERTEX_POINT('',#7352);
#2706=VERTEX_POINT('',#7356);
#2707=VERTEX_POINT('',#7357);
#2708=VERTEX_POINT('',#7359);
#2709=VERTEX_POINT('',#7364);
#2710=VERTEX_POINT('',#7369);
#2711=VERTEX_POINT('',#7370);
#2712=VERTEX_POINT('',#7378);
#2713=VERTEX_POINT('',#7379);
#2714=VERTEX_POINT('',#7383);
#2715=VERTEX_POINT('',#7388);
#2716=VERTEX_POINT('',#7395);
#2717=VERTEX_POINT('',#7396);
#2718=VERTEX_POINT('',#7398);
#2719=VERTEX_POINT('',#7400);
#2720=VERTEX_POINT('',#7407);
#2721=VERTEX_POINT('',#7408);
#2722=VERTEX_POINT('',#7410);
#2723=VERTEX_POINT('',#7427);
#2724=VERTEX_POINT('',#7428);
#2725=VERTEX_POINT('',#7441);
#2726=VERTEX_POINT('',#7453);
#2727=VERTEX_POINT('',#7454);
#2728=VERTEX_POINT('',#7456);
#2729=VERTEX_POINT('',#7473);
#2730=VERTEX_POINT('',#7474);
#2731=VERTEX_POINT('',#7487);
#2732=VERTEX_POINT('',#7500);
#2733=VERTEX_POINT('',#7502);
#2734=VERTEX_POINT('',#7518);
#2735=VERTEX_POINT('',#7520);
#2736=VERTEX_POINT('',#7556);
#2737=VERTEX_POINT('',#7558);
#2738=VERTEX_POINT('',#7561);
#2739=VERTEX_POINT('',#7563);
#2890=LINE('',#6904,#3068);
#2891=LINE('',#6907,#3069);
#2892=LINE('',#6911,#3070);
#2893=LINE('',#6913,#3071);
#2894=LINE('',#6921,#3072);
#2895=LINE('',#6924,#3073);
#2896=LINE('',#6932,#3074);
#2897=LINE('',#6934,#3075);
#2898=LINE('',#6938,#3076);
#2899=LINE('',#6941,#3077);
#2900=LINE('',#6943,#3078);
#2901=LINE('',#6945,#3079);
#2902=LINE('',#6947,#3080);
#2903=LINE('',#6950,#3081);
#2904=LINE('',#6952,#3082);
#2905=LINE('',#6954,#3083);
#2906=LINE('',#6956,#3084);
#2907=LINE('',#6961,#3085);
#2908=LINE('',#7011,#3086);
#2909=LINE('',#7016,#3087);
#2910=LINE('',#7020,#3088);
#2911=LINE('',#7021,#3089);
#2912=LINE('',#7026,#3090);
#2913=LINE('',#7030,#3091);
#2914=LINE('',#7032,#3092);
#2915=LINE('',#7033,#3093);
#2916=LINE('',#7069,#3094);
#2917=LINE('',#7078,#3095);
#2918=LINE('',#7086,#3096);
#2919=LINE('',#7095,#3097);
#2920=LINE('',#7108,#3098);
#2921=LINE('',#7118,#3099);
#2922=LINE('',#7133,#3100);
#2923=LINE('',#7158,#3101);
#2924=LINE('',#7172,#3102);
#2925=LINE('',#7181,#3103);
#2926=LINE('',#7191,#3104);
#2927=LINE('',#7200,#3105);
#2928=LINE('',#7208,#3106);
#2929=LINE('',#7217,#3107);
#2930=LINE('',#7228,#3108);
#2931=LINE('',#7240,#3109);
#2932=LINE('',#7256,#3110);
#2933=LINE('',#7268,#3111);
#2934=LINE('',#7278,#3112);
#2935=LINE('',#7279,#3113);
#2936=LINE('',#7281,#3114);
#2937=LINE('',#7282,#3115);
#2938=LINE('',#7289,#3116);
#2939=LINE('',#7292,#3117);
#2940=LINE('',#7294,#3118);
#2941=LINE('',#7296,#3119);
#2942=LINE('',#7307,#3120);
#2943=LINE('',#7321,#3121);
#2944=LINE('',#7324,#3122);
#2945=LINE('',#7325,#3123);
#2946=LINE('',#7337,#3124);
#2947=LINE('',#7342,#3125);
#2948=LINE('',#7346,#3126);
#2949=LINE('',#7349,#3127);
#2950=LINE('',#7351,#3128);
#2951=LINE('',#7353,#3129);
#2952=LINE('',#7355,#3130);
#2953=LINE('',#7368,#3131);
#2954=LINE('',#7371,#3132);
#2955=LINE('',#7372,#3133);
#2956=LINE('',#7394,#3134);
#2957=LINE('',#7399,#3135);
#2958=LINE('',#7429,#3136);
#2959=LINE('',#7475,#3137);
#3068=VECTOR('',#5456,1.);
#3069=VECTOR('',#5457,1.);
#3070=VECTOR('',#5460,1.);
#3071=VECTOR('',#5461,1.);
#3072=VECTOR('',#5470,1.);
#3073=VECTOR('',#5471,1.);
#3074=VECTOR('',#5478,1.);
#3075=VECTOR('',#5479,1.);
#3076=VECTOR('',#5484,1.);
#3077=VECTOR('',#5485,1.);
#3078=VECTOR('',#5486,1.);
#3079=VECTOR('',#5487,1.);
#3080=VECTOR('',#5490,1.);
#3081=VECTOR('',#5491,1.);
#3082=VECTOR('',#5492,1.);
#3083=VECTOR('',#5493,1.);
#3084=VECTOR('',#5496,1.);
#3085=VECTOR('',#5499,1.);
#3086=VECTOR('',#5512,1.);
#3087=VECTOR('',#5515,1.);
#3088=VECTOR('',#5520,1.);
#3089=VECTOR('',#5521,1.);
#3090=VECTOR('',#5526,1.);
#3091=VECTOR('',#5529,1.);
#3092=VECTOR('',#5532,1.);
#3093=VECTOR('',#5533,1.);
#3094=VECTOR('',#5564,1.);
#3095=VECTOR('',#5571,1.);
#3096=VECTOR('',#5580,1.);
#3097=VECTOR('',#5587,1.);
#3098=VECTOR('',#5600,1.);
#3099=VECTOR('',#5611,1.);
#3100=VECTOR('',#5616,1.);
#3101=VECTOR('',#5625,1.);
#3102=VECTOR('',#5630,1.);
#3103=VECTOR('',#5639,1.);
#3104=VECTOR('',#5650,1.);
#3105=VECTOR('',#5657,1.);
#3106=VECTOR('',#5666,1.);
#3107=VECTOR('',#5673,1.);
#3108=VECTOR('',#5684,1.);
#3109=VECTOR('',#5689,1.);
#3110=VECTOR('',#5702,1.);
#3111=VECTOR('',#5707,1.);
#3112=VECTOR('',#5712,1.);
#3113=VECTOR('',#5713,1.);
#3114=VECTOR('',#5716,1.);
#3115=VECTOR('',#5717,1.);
#3116=VECTOR('',#5726,1.);
#3117=VECTOR('',#5727,1.);
#3118=VECTOR('',#5728,1.);
#3119=VECTOR('',#5729,1.);
#3120=VECTOR('',#5736,1.);
#3121=VECTOR('',#5741,1.);
#3122=VECTOR('',#5742,1.);
#3123=VECTOR('',#5743,1.);
#3124=VECTOR('',#5754,1.);
#3125=VECTOR('',#5757,1.);
#3126=VECTOR('',#5762,1.);
#3127=VECTOR('',#5763,1.);
#3128=VECTOR('',#5764,1.);
#3129=VECTOR('',#5765,1.);
#3130=VECTOR('',#5768,1.);
#3131=VECTOR('',#5777,1.);
#3132=VECTOR('',#5778,1.);
#3133=VECTOR('',#5779,1.);
#3134=VECTOR('',#5790,1.);
#3135=VECTOR('',#5793,1.);
#3136=VECTOR('',#5802,1.);
#3137=VECTOR('',#5813,1.);
#3324=EDGE_LOOP('',(#999,#1000,#1001,#1002,#1003,#1004,#1005,#1006));
#3325=EDGE_LOOP('',(#1007,#1008,#1009,#1010,#1011,#1012,#1013,#1014));
#3326=EDGE_LOOP('',(#1015,#1016,#1017,#1018));
#3327=EDGE_LOOP('',(#1019,#1020,#1021,#1022));
#3328=EDGE_LOOP('',(#1023,#1024,#1025,#1026));
#3329=EDGE_LOOP('',(#1027));
#3330=EDGE_LOOP('',(#1028));
#3331=EDGE_LOOP('',(#1029));
#3332=EDGE_LOOP('',(#1030));
#3333=EDGE_LOOP('',(#1031,#1032,#1033,#1034));
#3334=EDGE_LOOP('',(#1035,#1036,#1037,#1038));
#3335=EDGE_LOOP('',(#1039,#1040,#1041,#1042));
#3336=EDGE_LOOP('',(#1043,#1044,#1045,#1046));
#3337=EDGE_LOOP('',(#1047,#1048,#1049,#1050));
#3338=EDGE_LOOP('',(#1051,#1052,#1053,#1054));
#3339=EDGE_LOOP('',(#1055,#1056,#1057,#1058));
#3340=EDGE_LOOP('',(#1059,#1060,#1061,#1062));
#3341=EDGE_LOOP('',(#1063,#1064,#1065,#1066));
#3342=EDGE_LOOP('',(#1067,#1068,#1069,#1070));
#3343=EDGE_LOOP('',(#1071,#1072,#1073,#1074,#1075,#1076,#1077,#1078));
#3344=EDGE_LOOP('',(#1079,#1080,#1081,#1082,#1083,#1084,#1085,#1086));
#3345=EDGE_LOOP('',(#1087,#1088,#1089,#1090,#1091,#1092));
#3346=EDGE_LOOP('',(#1093));
#3347=EDGE_LOOP('',(#1094,#1095,#1096,#1097,#1098,#1099,#1100,#1101));
#3348=EDGE_LOOP('',(#1102,#1103,#1104,#1105,#1106,#1107,#1108,#1109));
#3349=EDGE_LOOP('',(#1110,#1111,#1112,#1113,#1114,#1115));
#3350=EDGE_LOOP('',(#1116));
#3351=EDGE_LOOP('',(#1117,#1118,#1119,#1120,#1121,#1122,#1123,#1124));
#3352=EDGE_LOOP('',(#1125,#1126,#1127,#1128,#1129,#1130,#1131,#1132));
#3353=EDGE_LOOP('',(#1133));
#3354=EDGE_LOOP('',(#1134,#1135,#1136,#1137,#1138,#1139,#1140,#1141));
#3355=EDGE_LOOP('',(#1142,#1143,#1144,#1145));
#3356=EDGE_LOOP('',(#1146));
#3357=EDGE_LOOP('',(#1147,#1148,#1149,#1150,#1151,#1152,#1153,#1154));
#3358=EDGE_LOOP('',(#1155,#1156,#1157,#1158));
#3359=EDGE_LOOP('',(#1159,#1160,#1161,#1162));
#3360=EDGE_LOOP('',(#1163));
#3361=EDGE_LOOP('',(#1164));
#3362=EDGE_LOOP('',(#1165,#1166,#1167,#1168));
#3363=EDGE_LOOP('',(#1169,#1170,#1171,#1172,#1173,#1174,#1175,#1176));
#3364=EDGE_LOOP('',(#1177,#1178,#1179,#1180));
#3365=EDGE_LOOP('',(#1181,#1182,#1183,#1184,#1185,#1186));
#3366=EDGE_LOOP('',(#1187,#1188,#1189,#1190));
#3367=EDGE_LOOP('',(#1191,#1192,#1193,#1194));
#3368=EDGE_LOOP('',(#1195,#1196,#1197,#1198,#1199,#1200));
#3369=EDGE_LOOP('',(#1201,#1202,#1203,#1204));
#3370=EDGE_LOOP('',(#1205,#1206,#1207,#1208,#1209,#1210,#1211,#1212));
#3371=EDGE_LOOP('',(#1213,#1214,#1215,#1216));
#3372=EDGE_LOOP('',(#1217,#1218,#1219,#1220,#1221));
#3373=EDGE_LOOP('',(#1222,#1223,#1224,#1225));
#3374=EDGE_LOOP('',(#1226,#1227,#1228,#1229,#1230));
#3375=EDGE_LOOP('',(#1231,#1232,#1233,#1234,#1235));
#3376=EDGE_LOOP('',(#1236,#1237,#1238,#1239));
#3377=EDGE_LOOP('',(#1240,#1241,#1242,#1243,#1244));
#3378=EDGE_LOOP('',(#1245,#1246,#1247,#1248,#1249,#1250));
#3379=EDGE_LOOP('',(#1251,#1252,#1253,#1254,#1255,#1256));
#3380=EDGE_LOOP('',(#1257,#1258,#1259,#1260));
#3381=EDGE_LOOP('',(#1261,#1262,#1263,#1264));
#3382=EDGE_LOOP('',(#1265,#1266,#1267,#1268));
#3383=EDGE_LOOP('',(#1269,#1270,#1271,#1272));
#3384=EDGE_LOOP('',(#1273));
#3385=EDGE_LOOP('',(#1274));
#3386=EDGE_LOOP('',(#1275));
#3387=EDGE_LOOP('',(#1276));
#3388=EDGE_LOOP('',(#1277,#1278,#1279,#1280));
#3389=EDGE_LOOP('',(#1281,#1282,#1283,#1284));
#3390=EDGE_LOOP('',(#1285,#1286,#1287,#1288));
#3391=EDGE_LOOP('',(#1289,#1290,#1291,#1292));
#3392=EDGE_LOOP('',(#1293,#1294,#1295,#1296));
#3393=EDGE_LOOP('',(#1297,#1298,#1299,#1300));
#3394=EDGE_LOOP('',(#1301,#1302,#1303,#1304));
#3395=EDGE_LOOP('',(#1305,#1306,#1307,#1308));
#3396=EDGE_LOOP('',(#1309,#1310,#1311,#1312));
#3397=EDGE_LOOP('',(#1313,#1314,#1315,#1316));
#3398=EDGE_LOOP('',(#1317,#1318,#1319,#1320));
#3399=EDGE_LOOP('',(#1321,#1322,#1323,#1324));
#3400=EDGE_LOOP('',(#1325,#1326,#1327,#1328));
#3401=EDGE_LOOP('',(#1329,#1330,#1331,#1332));
#3402=EDGE_LOOP('',(#1333,#1334,#1335,#1336));
#3403=EDGE_LOOP('',(#1337,#1338,#1339,#1340));
#3404=EDGE_LOOP('',(#1341,#1342,#1343,#1344));
#3405=EDGE_LOOP('',(#1345,#1346,#1347,#1348));
#3406=EDGE_LOOP('',(#1349,#1350,#1351,#1352));
#3407=EDGE_LOOP('',(#1353,#1354,#1355,#1356));
#3408=EDGE_LOOP('',(#1357,#1358,#1359,#1360));
#3409=EDGE_LOOP('',(#1361,#1362,#1363,#1364));
#3410=EDGE_LOOP('',(#1365,#1366,#1367,#1368));
#3411=EDGE_LOOP('',(#1369,#1370,#1371,#1372));
#3412=EDGE_LOOP('',(#1373,#1374,#1375,#1376));
#3413=EDGE_LOOP('',(#1377,#1378,#1379,#1380));
#3414=EDGE_LOOP('',(#1381,#1382,#1383,#1384));
#3415=EDGE_LOOP('',(#1385,#1386,#1387,#1388));
#3416=EDGE_LOOP('',(#1389,#1390,#1391,#1392));
#3417=EDGE_LOOP('',(#1393,#1394,#1395,#1396));
#3418=EDGE_LOOP('',(#1397,#1398,#1399,#1400));
#3419=EDGE_LOOP('',(#1401,#1402,#1403,#1404));
#3420=EDGE_LOOP('',(#1405,#1406,#1407,#1408));
#3421=EDGE_LOOP('',(#1409,#1410,#1411,#1412));
#3422=EDGE_LOOP('',(#1413,#1414,#1415,#1416));
#3423=EDGE_LOOP('',(#1417,#1418,#1419,#1420));
#3424=EDGE_LOOP('',(#1421,#1422,#1423,#1424));
#3425=EDGE_LOOP('',(#1425,#1426,#1427,#1428));
#3426=EDGE_LOOP('',(#1429,#1430,#1431,#1432));
#3427=EDGE_LOOP('',(#1433,#1434,#1435,#1436));
#3428=EDGE_LOOP('',(#1437,#1438,#1439,#1440));
#3429=EDGE_LOOP('',(#1441,#1442,#1443,#1444));
#3430=EDGE_LOOP('',(#1445,#1446,#1447,#1448));
#3431=EDGE_LOOP('',(#1449,#1450,#1451,#1452));
#3432=EDGE_LOOP('',(#1453,#1454,#1455,#1456));
#3433=EDGE_LOOP('',(#1457,#1458,#1459,#1460));
#3434=EDGE_LOOP('',(#1461,#1462,#1463,#1464));
#3435=EDGE_LOOP('',(#1465,#1466,#1467,#1468));
#3436=EDGE_LOOP('',(#1469,#1470,#1471));
#3437=EDGE_LOOP('',(#1472,#1473,#1474,#1475));
#3438=EDGE_LOOP('',(#1476,#1477,#1478));
#3439=EDGE_LOOP('',(#1479,#1480,#1481));
#3440=EDGE_LOOP('',(#1482,#1483,#1484,#1485));
#3441=EDGE_LOOP('',(#1486,#1487,#1488));
#3442=EDGE_LOOP('',(#1489,#1490,#1491));
#3443=EDGE_LOOP('',(#1492,#1493,#1494,#1495));
#3444=EDGE_LOOP('',(#1496,#1497,#1498));
#3445=EDGE_LOOP('',(#1499,#1500,#1501));
#3446=EDGE_LOOP('',(#1502,#1503,#1504,#1505));
#3447=EDGE_LOOP('',(#1506,#1507,#1508));
#3448=EDGE_LOOP('',(#1509,#1510,#1511,#1512));
#3449=EDGE_LOOP('',(#1513,#1514,#1515,#1516));
#3450=EDGE_LOOP('',(#1517,#1518,#1519,#1520));
#3451=EDGE_LOOP('',(#1521,#1522,#1523));
#3452=EDGE_LOOP('',(#1524,#1525,#1526));
#3453=EDGE_LOOP('',(#1527,#1528,#1529,#1530));
#3454=EDGE_LOOP('',(#1531,#1532,#1533,#1534));
#3455=EDGE_LOOP('',(#1535,#1536,#1537,#1538));
#3456=EDGE_LOOP('',(#1539));
#3457=EDGE_LOOP('',(#1540));
#3458=EDGE_LOOP('',(#1541));
#3459=EDGE_LOOP('',(#1542));
#3460=EDGE_LOOP('',(#1543));
#3461=EDGE_LOOP('',(#1544));
#3462=EDGE_LOOP('',(#1545,#1546,#1547,#1548));
#3463=EDGE_LOOP('',(#1549,#1550,#1551,#1552));
#3464=EDGE_LOOP('',(#1553,#1554,#1555,#1556));
#3465=EDGE_LOOP('',(#1557,#1558,#1559));
#3466=EDGE_LOOP('',(#1560,#1561,#1562));
#3467=EDGE_LOOP('',(#1563,#1564,#1565,#1566));
#3468=EDGE_LOOP('',(#1567,#1568,#1569,#1570));
#3469=EDGE_LOOP('',(#1571,#1572,#1573,#1574));
#3470=EDGE_LOOP('',(#1575));
#3471=EDGE_LOOP('',(#1576));
#3472=EDGE_LOOP('',(#1577,#1578,#1579,#1580,#1581,#1582,#1583,#1584,#1585,
#1586,#1587,#1588));
#3473=EDGE_LOOP('',(#1589));
#3474=EDGE_LOOP('',(#1590,#1591,#1592,#1593,#1594,#1595,#1596,#1597,#1598,
#1599,#1600,#1601));
#3475=EDGE_LOOP('',(#1602));
#3701=FACE_BOUND('',#3324,.T.);
#3702=FACE_BOUND('',#3325,.T.);
#3703=FACE_BOUND('',#3326,.T.);
#3704=FACE_BOUND('',#3327,.T.);
#3705=FACE_BOUND('',#3328,.T.);
#3706=FACE_BOUND('',#3329,.T.);
#3707=FACE_BOUND('',#3330,.T.);
#3708=FACE_BOUND('',#3331,.T.);
#3709=FACE_BOUND('',#3332,.T.);
#3710=FACE_BOUND('',#3333,.T.);
#3711=FACE_BOUND('',#3334,.T.);
#3712=FACE_BOUND('',#3335,.T.);
#3713=FACE_BOUND('',#3336,.T.);
#3714=FACE_BOUND('',#3337,.T.);
#3715=FACE_BOUND('',#3338,.T.);
#3716=FACE_BOUND('',#3339,.T.);
#3717=FACE_BOUND('',#3340,.T.);
#3718=FACE_BOUND('',#3341,.T.);
#3719=FACE_BOUND('',#3342,.T.);
#3720=FACE_BOUND('',#3343,.T.);
#3721=FACE_BOUND('',#3344,.T.);
#3722=FACE_BOUND('',#3345,.T.);
#3723=FACE_BOUND('',#3346,.T.);
#3724=FACE_BOUND('',#3347,.T.);
#3725=FACE_BOUND('',#3348,.T.);
#3726=FACE_BOUND('',#3349,.T.);
#3727=FACE_BOUND('',#3350,.T.);
#3728=FACE_BOUND('',#3351,.T.);
#3729=FACE_BOUND('',#3352,.T.);
#3730=FACE_BOUND('',#3353,.T.);
#3731=FACE_BOUND('',#3354,.T.);
#3732=FACE_BOUND('',#3355,.T.);
#3733=FACE_BOUND('',#3356,.T.);
#3734=FACE_BOUND('',#3357,.T.);
#3735=FACE_BOUND('',#3358,.T.);
#3736=FACE_BOUND('',#3359,.T.);
#3737=FACE_BOUND('',#3360,.T.);
#3738=FACE_BOUND('',#3361,.T.);
#3739=FACE_BOUND('',#3362,.T.);
#3740=FACE_BOUND('',#3363,.T.);
#3741=FACE_BOUND('',#3364,.T.);
#3742=FACE_BOUND('',#3365,.T.);
#3743=FACE_BOUND('',#3366,.T.);
#3744=FACE_BOUND('',#3367,.T.);
#3745=FACE_BOUND('',#3368,.T.);
#3746=FACE_BOUND('',#3369,.T.);
#3747=FACE_BOUND('',#3370,.T.);
#3748=FACE_BOUND('',#3371,.T.);
#3749=FACE_BOUND('',#3372,.T.);
#3750=FACE_BOUND('',#3373,.T.);
#3751=FACE_BOUND('',#3374,.T.);
#3752=FACE_BOUND('',#3375,.T.);
#3753=FACE_BOUND('',#3376,.T.);
#3754=FACE_BOUND('',#3377,.T.);
#3755=FACE_BOUND('',#3378,.T.);
#3756=FACE_BOUND('',#3379,.T.);
#3757=FACE_BOUND('',#3380,.T.);
#3758=FACE_BOUND('',#3381,.T.);
#3759=FACE_BOUND('',#3382,.T.);
#3760=FACE_BOUND('',#3383,.T.);
#3761=FACE_BOUND('',#3384,.T.);
#3762=FACE_BOUND('',#3385,.T.);
#3763=FACE_BOUND('',#3386,.T.);
#3764=FACE_BOUND('',#3387,.T.);
#3765=FACE_BOUND('',#3388,.T.);
#3766=FACE_BOUND('',#3389,.T.);
#3767=FACE_BOUND('',#3390,.T.);
#3768=FACE_BOUND('',#3391,.T.);
#3769=FACE_BOUND('',#3392,.T.);
#3770=FACE_BOUND('',#3393,.T.);
#3771=FACE_BOUND('',#3394,.T.);
#3772=FACE_BOUND('',#3395,.T.);
#3773=FACE_BOUND('',#3396,.T.);
#3774=FACE_BOUND('',#3397,.T.);
#3775=FACE_BOUND('',#3398,.T.);
#3776=FACE_BOUND('',#3399,.T.);
#3777=FACE_BOUND('',#3400,.T.);
#3778=FACE_BOUND('',#3401,.T.);
#3779=FACE_BOUND('',#3402,.T.);
#3780=FACE_BOUND('',#3403,.T.);
#3781=FACE_BOUND('',#3404,.T.);
#3782=FACE_BOUND('',#3405,.T.);
#3783=FACE_BOUND('',#3406,.T.);
#3784=FACE_BOUND('',#3407,.T.);
#3785=FACE_BOUND('',#3408,.T.);
#3786=FACE_BOUND('',#3409,.T.);
#3787=FACE_BOUND('',#3410,.T.);
#3788=FACE_BOUND('',#3411,.T.);
#3789=FACE_BOUND('',#3412,.T.);
#3790=FACE_BOUND('',#3413,.T.);
#3791=FACE_BOUND('',#3414,.T.);
#3792=FACE_BOUND('',#3415,.T.);
#3793=FACE_BOUND('',#3416,.T.);
#3794=FACE_BOUND('',#3417,.T.);
#3795=FACE_BOUND('',#3418,.T.);
#3796=FACE_BOUND('',#3419,.T.);
#3797=FACE_BOUND('',#3420,.T.);
#3798=FACE_BOUND('',#3421,.T.);
#3799=FACE_BOUND('',#3422,.T.);
#3800=FACE_BOUND('',#3423,.T.);
#3801=FACE_BOUND('',#3424,.T.);
#3802=FACE_BOUND('',#3425,.T.);
#3803=FACE_BOUND('',#3426,.T.);
#3804=FACE_BOUND('',#3427,.T.);
#3805=FACE_BOUND('',#3428,.T.);
#3806=FACE_BOUND('',#3429,.T.);
#3807=FACE_BOUND('',#3430,.T.);
#3808=FACE_BOUND('',#3431,.T.);
#3809=FACE_BOUND('',#3432,.T.);
#3810=FACE_BOUND('',#3433,.T.);
#3811=FACE_BOUND('',#3434,.T.);
#3812=FACE_BOUND('',#3435,.T.);
#3813=FACE_BOUND('',#3436,.T.);
#3814=FACE_BOUND('',#3437,.T.);
#3815=FACE_BOUND('',#3438,.T.);
#3816=FACE_BOUND('',#3439,.T.);
#3817=FACE_BOUND('',#3440,.T.);
#3818=FACE_BOUND('',#3441,.T.);
#3819=FACE_BOUND('',#3442,.T.);
#3820=FACE_BOUND('',#3443,.T.);
#3821=FACE_BOUND('',#3444,.T.);
#3822=FACE_BOUND('',#3445,.T.);
#3823=FACE_BOUND('',#3446,.T.);
#3824=FACE_BOUND('',#3447,.T.);
#3825=FACE_BOUND('',#3448,.T.);
#3826=FACE_BOUND('',#3449,.T.);
#3827=FACE_BOUND('',#3450,.T.);
#3828=FACE_BOUND('',#3451,.T.);
#3829=FACE_BOUND('',#3452,.T.);
#3830=FACE_BOUND('',#3453,.T.);
#3831=FACE_BOUND('',#3454,.T.);
#3832=FACE_BOUND('',#3455,.T.);
#3833=FACE_BOUND('',#3456,.T.);
#3834=FACE_BOUND('',#3457,.T.);
#3835=FACE_BOUND('',#3458,.T.);
#3836=FACE_BOUND('',#3459,.T.);
#3837=FACE_BOUND('',#3460,.T.);
#3838=FACE_BOUND('',#3461,.T.);
#3839=FACE_BOUND('',#3462,.T.);
#3840=FACE_BOUND('',#3463,.T.);
#3841=FACE_BOUND('',#3464,.T.);
#3842=FACE_BOUND('',#3465,.T.);
#3843=FACE_BOUND('',#3466,.T.);
#3844=FACE_BOUND('',#3467,.T.);
#3845=FACE_BOUND('',#3468,.T.);
#3846=FACE_BOUND('',#3469,.T.);
#3847=FACE_BOUND('',#3470,.T.);
#3848=FACE_BOUND('',#3471,.T.);
#3849=FACE_BOUND('',#3472,.T.);
#3850=FACE_BOUND('',#3473,.T.);
#3851=FACE_BOUND('',#3474,.T.);
#3852=FACE_BOUND('',#3475,.T.);
#3984=PLANE('',#4651);
#3985=PLANE('',#4656);
#3986=PLANE('',#4661);
#3987=PLANE('',#4662);
#3988=PLANE('',#4673);
#3989=PLANE('',#4677);
#3990=PLANE('',#4692);
#3991=PLANE('',#4699);
#3992=PLANE('',#4706);
#3993=PLANE('',#4723);
#3994=PLANE('',#4730);
#3995=PLANE('',#4737);
#3996=PLANE('',#4757);
#3997=PLANE('',#4758);
#3998=PLANE('',#4762);
#3999=PLANE('',#4767);
#4000=PLANE('',#4772);
#4001=PLANE('',#4775);
#4002=PLANE('',#4780);
#4003=PLANE('',#4785);
#4004=PLANE('',#4806);
#4005=PLANE('',#4809);
#4006=PLANE('',#4938);
#4007=PLANE('',#4939);
#4123=ADVANCED_FACE('',(#3701),#3984,.T.);
#4124=ADVANCED_FACE('',(#3702),#3985,.F.);
#4125=ADVANCED_FACE('',(#3703),#3986,.F.);
#4126=ADVANCED_FACE('',(#3704),#3987,.T.);
#4127=ADVANCED_FACE('',(#3705),#239,.F.);
#4128=ADVANCED_FACE('',(#3706,#3707),#240,.F.);
#4129=ADVANCED_FACE('',(#3708,#3709),#241,.F.);
#4130=ADVANCED_FACE('',(#3710),#242,.T.);
#4131=ADVANCED_FACE('',(#3711),#3988,.T.);
#4132=ADVANCED_FACE('',(#3712),#243,.T.);
#4133=ADVANCED_FACE('',(#3713),#3989,.T.);
#4134=ADVANCED_FACE('',(#3714),#244,.T.);
#4135=ADVANCED_FACE('',(#3715),#245,.T.);
#4136=ADVANCED_FACE('',(#3716),#246,.T.);
#4137=ADVANCED_FACE('',(#3717),#247,.T.);
#4138=ADVANCED_FACE('',(#3718),#144,.F.);
#4139=ADVANCED_FACE('',(#3719),#145,.F.);
#4140=ADVANCED_FACE('',(#3720),#3990,.F.);
#4141=ADVANCED_FACE('',(#3721),#3991,.T.);
#4142=ADVANCED_FACE('',(#3722,#3723),#3992,.T.);
#4143=ADVANCED_FACE('',(#3724),#248,.F.);
#4144=ADVANCED_FACE('',(#3725),#249,.F.);
#4145=ADVANCED_FACE('',(#3726,#3727),#3993,.F.);
#4146=ADVANCED_FACE('',(#3728),#3994,.F.);
#4147=ADVANCED_FACE('',(#3729),#3995,.T.);
#4148=ADVANCED_FACE('',(#3730,#3731),#250,.F.);
#4149=ADVANCED_FACE('',(#3732),#251,.T.);
#4150=ADVANCED_FACE('',(#3733,#3734),#252,.F.);
#4151=ADVANCED_FACE('',(#3735),#3996,.F.);
#4152=ADVANCED_FACE('',(#3736),#3997,.T.);
#4153=ADVANCED_FACE('',(#3737,#3738),#253,.F.);
#4154=ADVANCED_FACE('',(#3739),#3998,.F.);
#4155=ADVANCED_FACE('',(#3740),#254,.F.);
#4156=ADVANCED_FACE('',(#3741),#3999,.T.);
#4157=ADVANCED_FACE('',(#3742),#255,.F.);
#4158=ADVANCED_FACE('',(#3743),#4000,.T.);
#4159=ADVANCED_FACE('',(#3744),#4001,.T.);
#4160=ADVANCED_FACE('',(#3745),#256,.F.);
#4161=ADVANCED_FACE('',(#3746),#4002,.F.);
#4162=ADVANCED_FACE('',(#3747),#257,.F.);
#4163=ADVANCED_FACE('',(#3748),#4003,.T.);
#4164=ADVANCED_FACE('',(#3749),#146,.F.);
#4165=ADVANCED_FACE('',(#3750),#258,.F.);
#4166=ADVANCED_FACE('',(#3751),#147,.F.);
#4167=ADVANCED_FACE('',(#3752),#148,.F.);
#4168=ADVANCED_FACE('',(#3753),#259,.F.);
#4169=ADVANCED_FACE('',(#3754),#149,.F.);
#4170=ADVANCED_FACE('',(#3755),#150,.F.);
#4171=ADVANCED_FACE('',(#3756),#151,.F.);
#4172=ADVANCED_FACE('',(#3757),#152,.F.);
#4173=ADVANCED_FACE('',(#3758),#260,.F.);
#4174=ADVANCED_FACE('',(#3759),#261,.F.);
#4175=ADVANCED_FACE('',(#3760),#153,.F.);
#4176=ADVANCED_FACE('',(#3761,#3762),#4004,.T.);
#4177=ADVANCED_FACE('',(#3763,#3764),#4005,.T.);
#4178=ADVANCED_FACE('',(#3765),#154,.T.);
#4179=ADVANCED_FACE('',(#3766),#262,.T.);
#4180=ADVANCED_FACE('',(#3767),#27,.T.);
#4181=ADVANCED_FACE('',(#3768),#155,.T.);
#4182=ADVANCED_FACE('',(#3769),#156,.T.);
#4183=ADVANCED_FACE('',(#3770),#28,.T.);
#4184=ADVANCED_FACE('',(#3771),#263,.T.);
#4185=ADVANCED_FACE('',(#3772),#264,.T.);
#4186=ADVANCED_FACE('',(#3773),#157,.T.);
#4187=ADVANCED_FACE('',(#3774),#29,.T.);
#4188=ADVANCED_FACE('',(#3775),#158,.T.);
#4189=ADVANCED_FACE('',(#3776),#30,.T.);
#4190=ADVANCED_FACE('',(#3777),#159,.T.);
#4191=ADVANCED_FACE('',(#3778),#265,.T.);
#4192=ADVANCED_FACE('',(#3779),#160,.T.);
#4193=ADVANCED_FACE('',(#3780),#31,.T.);
#4194=ADVANCED_FACE('',(#3781),#161,.T.);
#4195=ADVANCED_FACE('',(#3782),#32,.T.);
#4196=ADVANCED_FACE('',(#3783),#162,.T.);
#4197=ADVANCED_FACE('',(#3784),#266,.T.);
#4198=ADVANCED_FACE('',(#3785),#163,.T.);
#4199=ADVANCED_FACE('',(#3786),#33,.T.);
#4200=ADVANCED_FACE('',(#3787),#164,.T.);
#4201=ADVANCED_FACE('',(#3788),#267,.T.);
#4202=ADVANCED_FACE('',(#3789),#34,.T.);
#4203=ADVANCED_FACE('',(#3790),#165,.T.);
#4204=ADVANCED_FACE('',(#3791),#166,.T.);
#4205=ADVANCED_FACE('',(#3792),#35,.T.);
#4206=ADVANCED_FACE('',(#3793),#268,.T.);
#4207=ADVANCED_FACE('',(#3794),#167,.F.);
#4208=ADVANCED_FACE('',(#3795),#168,.T.);
#4209=ADVANCED_FACE('',(#3796),#36,.T.);
#4210=ADVANCED_FACE('',(#3797),#169,.T.);
#4211=ADVANCED_FACE('',(#3798),#37,.T.);
#4212=ADVANCED_FACE('',(#3799),#170,.T.);
#4213=ADVANCED_FACE('',(#3800),#269,.T.);
#4214=ADVANCED_FACE('',(#3801),#171,.T.);
#4215=ADVANCED_FACE('',(#3802),#38,.T.);
#4216=ADVANCED_FACE('',(#3803),#172,.T.);
#4217=ADVANCED_FACE('',(#3804),#39,.T.);
#4218=ADVANCED_FACE('',(#3805),#173,.T.);
#4219=ADVANCED_FACE('',(#3806),#270,.T.);
#4220=ADVANCED_FACE('',(#3807),#174,.T.);
#4221=ADVANCED_FACE('',(#3808),#40,.T.);
#4222=ADVANCED_FACE('',(#3809),#175,.F.);
#4223=ADVANCED_FACE('',(#3810),#271,.F.);
#4224=ADVANCED_FACE('',(#3811),#272,.F.);
#4225=ADVANCED_FACE('',(#3812),#176,.F.);
#4226=ADVANCED_FACE('',(#3813),#15,.T.);
#4227=ADVANCED_FACE('',(#3814),#177,.T.);
#4228=ADVANCED_FACE('',(#3815),#16,.T.);
#4229=ADVANCED_FACE('',(#3816),#17,.T.);
#4230=ADVANCED_FACE('',(#3817),#273,.T.);
#4231=ADVANCED_FACE('',(#3818),#18,.T.);
#4232=ADVANCED_FACE('',(#3819),#19,.T.);
#4233=ADVANCED_FACE('',(#3820),#274,.T.);
#4234=ADVANCED_FACE('',(#3821),#20,.T.);
#4235=ADVANCED_FACE('',(#3822),#21,.T.);
#4236=ADVANCED_FACE('',(#3823),#178,.T.);
#4237=ADVANCED_FACE('',(#3824),#22,.T.);
#4238=ADVANCED_FACE('',(#3825),#179,.T.);
#4239=ADVANCED_FACE('',(#3826),#180,.T.);
#4240=ADVANCED_FACE('',(#3827),#181,.T.);
#4241=ADVANCED_FACE('',(#3828),#23,.T.);
#4242=ADVANCED_FACE('',(#3829),#24,.T.);
#4243=ADVANCED_FACE('',(#3830),#182,.T.);
#4244=ADVANCED_FACE('',(#3831),#183,.T.);
#4245=ADVANCED_FACE('',(#3832),#275,.T.);
#4246=ADVANCED_FACE('',(#3833,#3834),#184,.F.);
#4247=ADVANCED_FACE('',(#3835,#3836),#185,.T.);
#4248=ADVANCED_FACE('',(#3837,#3838),#186,.T.);
#4249=ADVANCED_FACE('',(#3839),#187,.T.);
#4250=ADVANCED_FACE('',(#3840),#188,.T.);
#4251=ADVANCED_FACE('',(#3841),#189,.T.);
#4252=ADVANCED_FACE('',(#3842),#25,.T.);
#4253=ADVANCED_FACE('',(#3843),#26,.T.);
#4254=ADVANCED_FACE('',(#3844),#190,.T.);
#4255=ADVANCED_FACE('',(#3845),#191,.T.);
#4256=ADVANCED_FACE('',(#3846),#276,.T.);
#4257=ADVANCED_FACE('',(#3847,#3848),#192,.F.);
#4258=ADVANCED_FACE('',(#3849,#3850),#4006,.T.);
#4259=ADVANCED_FACE('',(#3851,#3852),#4007,.T.);
#4329=CLOSED_SHELL('',(#4123,#4124,#4125,#4126,#4127,#4128,#4129,#4130,
#4131,#4132,#4133,#4134,#4135,#4136,#4137,#4138,#4139,#4140,#4141,#4142,
#4143,#4144,#4145,#4146,#4147,#4148,#4149,#4150,#4151,#4152,#4153,#4154,
#4155,#4156,#4157,#4158,#4159,#4160,#4161,#4162,#4163,#4164,#4165,#4166,
#4167,#4168,#4169,#4170,#4171,#4172,#4173,#4174,#4175,#4176,#4177,#4178,
#4179,#4180,#4181,#4182,#4183,#4184,#4185,#4186,#4187,#4188,#4189,#4190,
#4191,#4192,#4193,#4194,#4195,#4196,#4197,#4198,#4199,#4200,#4201,#4202,
#4203,#4204,#4205,#4206,#4207,#4208,#4209,#4210,#4211,#4212,#4213,#4214,
#4215,#4216,#4217,#4218,#4219,#4220,#4221,#4222,#4223,#4224,#4225,#4226,
#4227,#4228,#4229,#4230,#4231,#4232,#4233,#4234,#4235,#4236,#4237,#4238,
#4239,#4240,#4241,#4242,#4243,#4244,#4245,#4246,#4247,#4248,#4249,#4250,
#4251,#4252,#4253,#4254,#4255,#4256,#4257,#4258,#4259));
#4340=STYLED_ITEM('',(#4351),#4455);
#4351=PRESENTATION_STYLE_ASSIGNMENT((#4367));
#4367=SURFACE_STYLE_USAGE(.BOTH.,#4383);
#4383=SURFACE_SIDE_STYLE('',(#4399));
#4399=SURFACE_STYLE_FILL_AREA(#4415);
#4415=FILL_AREA_STYLE('',(#4431));
#4431=FILL_AREA_STYLE_COLOUR('',#4442);
#4442=COLOUR_RGB('', 0.31764706, 0.68627451, 0.89019608);
#4455=MANIFOLD_SOLID_BREP('Part 1',#4329);
#4467=SHAPE_DEFINITION_REPRESENTATION(#8578,#4479);
#4479=SHAPE_REPRESENTATION('Part 1',(#4484),#8542);
#4484=AXIS2_PLACEMENT_3D('',#6402,#5064,#5065);
#4651=AXIS2_PLACEMENT_3D('',#6903,#5454,#5455);
#4652=AXIS2_PLACEMENT_3D('',#6909,#5458,#5459);
#4653=AXIS2_PLACEMENT_3D('',#6915,#5462,#5463);
#4654=AXIS2_PLACEMENT_3D('',#6917,#5464,#5465);
#4655=AXIS2_PLACEMENT_3D('',#6919,#5466,#5467);
#4656=AXIS2_PLACEMENT_3D('',#6920,#5468,#5469);
#4657=AXIS2_PLACEMENT_3D('',#6926,#5472,#5473);
#4658=AXIS2_PLACEMENT_3D('',#6928,#5474,#5475);
#4659=AXIS2_PLACEMENT_3D('',#6930,#5476,#5477);
#4660=AXIS2_PLACEMENT_3D('',#6936,#5480,#5481);
#4661=AXIS2_PLACEMENT_3D('',#6937,#5482,#5483);
#4662=AXIS2_PLACEMENT_3D('',#6946,#5488,#5489);
#4663=AXIS2_PLACEMENT_3D('',#6955,#5494,#5495);
#4664=AXIS2_PLACEMENT_3D('',#6959,#5497,#5498);
#4665=AXIS2_PLACEMENT_3D('',#6963,#5500,#5501);
#4666=AXIS2_PLACEMENT_3D('',#6964,#5502,#5503);
#4667=AXIS2_PLACEMENT_3D('',#6985,#5504,#5505);
#4668=AXIS2_PLACEMENT_3D('',#6987,#5506,#5507);
#4669=AXIS2_PLACEMENT_3D('',#7008,#5508,#5509);
#4670=AXIS2_PLACEMENT_3D('',#7010,#5510,#5511);
#4671=AXIS2_PLACEMENT_3D('',#7014,#5513,#5514);
#4672=AXIS2_PLACEMENT_3D('',#7018,#5516,#5517);
#4673=AXIS2_PLACEMENT_3D('',#7019,#5518,#5519);
#4674=AXIS2_PLACEMENT_3D('',#7022,#5522,#5523);
#4675=AXIS2_PLACEMENT_3D('',#7023,#5524,#5525);
#4676=AXIS2_PLACEMENT_3D('',#7028,#5527,#5528);
#4677=AXIS2_PLACEMENT_3D('',#7031,#5530,#5531);
#4678=AXIS2_PLACEMENT_3D('',#7034,#5534,#5535);
#4679=AXIS2_PLACEMENT_3D('',#7035,#5536,#5537);
#4680=AXIS2_PLACEMENT_3D('',#7036,#5538,#5539);
#4681=AXIS2_PLACEMENT_3D('',#7037,#5540,#5541);
#4682=AXIS2_PLACEMENT_3D('',#7038,#5542,#5543);
#4683=AXIS2_PLACEMENT_3D('',#7039,#5544,#5545);
#4684=AXIS2_PLACEMENT_3D('',#7040,#5546,#5547);
#4685=AXIS2_PLACEMENT_3D('',#7041,#5548,#5549);
#4686=AXIS2_PLACEMENT_3D('',#7042,#5550,#5551);
#4687=AXIS2_PLACEMENT_3D('',#7043,#5552,#5553);
#4688=AXIS2_PLACEMENT_3D('',#7044,#5554,#5555);
#4689=AXIS2_PLACEMENT_3D('',#7045,#5556,#5557);
#4690=AXIS2_PLACEMENT_3D('',#7046,#5558,#5559);
#4691=AXIS2_PLACEMENT_3D('',#7057,#5560,#5561);
#4692=AXIS2_PLACEMENT_3D('',#7068,#5562,#5563);
#4693=AXIS2_PLACEMENT_3D('',#7072,#5565,#5566);
#4694=AXIS2_PLACEMENT_3D('',#7074,#5567,#5568);
#4695=AXIS2_PLACEMENT_3D('',#7076,#5569,#5570);
#4696=AXIS2_PLACEMENT_3D('',#7080,#5572,#5573);
#4697=AXIS2_PLACEMENT_3D('',#7082,#5574,#5575);
#4698=AXIS2_PLACEMENT_3D('',#7084,#5576,#5577);
#4699=AXIS2_PLACEMENT_3D('',#7085,#5578,#5579);
#4700=AXIS2_PLACEMENT_3D('',#7089,#5581,#5582);
#4701=AXIS2_PLACEMENT_3D('',#7091,#5583,#5584);
#4702=AXIS2_PLACEMENT_3D('',#7093,#5585,#5586);
#4703=AXIS2_PLACEMENT_3D('',#7097,#5588,#5589);
#4704=AXIS2_PLACEMENT_3D('',#7099,#5590,#5591);
#4705=AXIS2_PLACEMENT_3D('',#7101,#5592,#5593);
#4706=AXIS2_PLACEMENT_3D('',#7102,#5594,#5595);
#4707=AXIS2_PLACEMENT_3D('',#7103,#5596,#5597);
#4708=AXIS2_PLACEMENT_3D('',#7106,#5598,#5599);
#4709=AXIS2_PLACEMENT_3D('',#7110,#5601,#5602);
#4710=AXIS2_PLACEMENT_3D('',#7112,#5603,#5604);
#4711=AXIS2_PLACEMENT_3D('',#7114,#5605,#5606);
#4712=AXIS2_PLACEMENT_3D('',#7115,#5607,#5608);
#4713=AXIS2_PLACEMENT_3D('',#7117,#5609,#5610);
#4714=AXIS2_PLACEMENT_3D('',#7121,#5612,#5613);
#4715=AXIS2_PLACEMENT_3D('',#7131,#5614,#5615);
#4716=AXIS2_PLACEMENT_3D('',#7135,#5617,#5618);
#4717=AXIS2_PLACEMENT_3D('',#7145,#5619,#5620);
#4718=AXIS2_PLACEMENT_3D('',#7146,#5621,#5622);
#4719=AXIS2_PLACEMENT_3D('',#7156,#5623,#5624);
#4720=AXIS2_PLACEMENT_3D('',#7160,#5626,#5627);
#4721=AXIS2_PLACEMENT_3D('',#7170,#5628,#5629);
#4722=AXIS2_PLACEMENT_3D('',#7174,#5631,#5632);
#4723=AXIS2_PLACEMENT_3D('',#7175,#5633,#5634);
#4724=AXIS2_PLACEMENT_3D('',#7176,#5635,#5636);
#4725=AXIS2_PLACEMENT_3D('',#7179,#5637,#5638);
#4726=AXIS2_PLACEMENT_3D('',#7183,#5640,#5641);
#4727=AXIS2_PLACEMENT_3D('',#7185,#5642,#5643);
#4728=AXIS2_PLACEMENT_3D('',#7187,#5644,#5645);
#4729=AXIS2_PLACEMENT_3D('',#7188,#5646,#5647);
#4730=AXIS2_PLACEMENT_3D('',#7190,#5648,#5649);
#4731=AXIS2_PLACEMENT_3D('',#7194,#5651,#5652);
#4732=AXIS2_PLACEMENT_3D('',#7196,#5653,#5654);
#4733=AXIS2_PLACEMENT_3D('',#7198,#5655,#5656);
#4734=AXIS2_PLACEMENT_3D('',#7202,#5658,#5659);
#4735=AXIS2_PLACEMENT_3D('',#7204,#5660,#5661);
#4736=AXIS2_PLACEMENT_3D('',#7206,#5662,#5663);
#4737=AXIS2_PLACEMENT_3D('',#7207,#5664,#5665);
#4738=AXIS2_PLACEMENT_3D('',#7211,#5667,#5668);
#4739=AXIS2_PLACEMENT_3D('',#7213,#5669,#5670);
#4740=AXIS2_PLACEMENT_3D('',#7215,#5671,#5672);
#4741=AXIS2_PLACEMENT_3D('',#7219,#5674,#5675);
#4742=AXIS2_PLACEMENT_3D('',#7221,#5676,#5677);
#4743=AXIS2_PLACEMENT_3D('',#7223,#5678,#5679);
#4744=AXIS2_PLACEMENT_3D('',#7224,#5680,#5681);
#4745=AXIS2_PLACEMENT_3D('',#7225,#5682,#5683);
#4746=AXIS2_PLACEMENT_3D('',#7230,#5685,#5686);
#4747=AXIS2_PLACEMENT_3D('',#7238,#5687,#5688);
#4748=AXIS2_PLACEMENT_3D('',#7242,#5690,#5691);
#4749=AXIS2_PLACEMENT_3D('',#7249,#5692,#5693);
#4750=AXIS2_PLACEMENT_3D('',#7250,#5694,#5695);
#4751=AXIS2_PLACEMENT_3D('',#7251,#5696,#5697);
#4752=AXIS2_PLACEMENT_3D('',#7252,#5698,#5699);
#4753=AXIS2_PLACEMENT_3D('',#7253,#5700,#5701);
#4754=AXIS2_PLACEMENT_3D('',#7258,#5703,#5704);
#4755=AXIS2_PLACEMENT_3D('',#7266,#5705,#5706);
#4756=AXIS2_PLACEMENT_3D('',#7270,#5708,#5709);
#4757=AXIS2_PLACEMENT_3D('',#7277,#5710,#5711);
#4758=AXIS2_PLACEMENT_3D('',#7280,#5714,#5715);
#4759=AXIS2_PLACEMENT_3D('',#7283,#5718,#5719);
#4760=AXIS2_PLACEMENT_3D('',#7284,#5720,#5721);
#4761=AXIS2_PLACEMENT_3D('',#7286,#5722,#5723);
#4762=AXIS2_PLACEMENT_3D('',#7288,#5724,#5725);
#4763=AXIS2_PLACEMENT_3D('',#7297,#5730,#5731);
#4764=AXIS2_PLACEMENT_3D('',#7304,#5732,#5733);
#4765=AXIS2_PLACEMENT_3D('',#7305,#5734,#5735);
#4766=AXIS2_PLACEMENT_3D('',#7309,#5737,#5738);
#4767=AXIS2_PLACEMENT_3D('',#7320,#5739,#5740);
#4768=AXIS2_PLACEMENT_3D('',#7326,#5744,#5745);
#4769=AXIS2_PLACEMENT_3D('',#7327,#5746,#5747);
#4770=AXIS2_PLACEMENT_3D('',#7334,#5748,#5749);
#4771=AXIS2_PLACEMENT_3D('',#7335,#5750,#5751);
#4772=AXIS2_PLACEMENT_3D('',#7336,#5752,#5753);
#4773=AXIS2_PLACEMENT_3D('',#7340,#5755,#5756);
#4774=AXIS2_PLACEMENT_3D('',#7344,#5758,#5759);
#4775=AXIS2_PLACEMENT_3D('',#7345,#5760,#5761);
#4776=AXIS2_PLACEMENT_3D('',#7354,#5766,#5767);
#4777=AXIS2_PLACEMENT_3D('',#7358,#5769,#5770);
#4778=AXIS2_PLACEMENT_3D('',#7365,#5771,#5772);
#4779=AXIS2_PLACEMENT_3D('',#7366,#5773,#5774);
#4780=AXIS2_PLACEMENT_3D('',#7367,#5775,#5776);
#4781=AXIS2_PLACEMENT_3D('',#7373,#5780,#5781);
#4782=AXIS2_PLACEMENT_3D('',#7380,#5782,#5783);
#4783=AXIS2_PLACEMENT_3D('',#7381,#5784,#5785);
#4784=AXIS2_PLACEMENT_3D('',#7382,#5786,#5787);
#4785=AXIS2_PLACEMENT_3D('',#7393,#5788,#5789);
#4786=AXIS2_PLACEMENT_3D('',#7397,#5791,#5792);
#4787=AXIS2_PLACEMENT_3D('',#7401,#5794,#5795);
#4788=AXIS2_PLACEMENT_3D('',#7402,#5796,#5797);
#4789=AXIS2_PLACEMENT_3D('',#7409,#5798,#5799);
#4790=AXIS2_PLACEMENT_3D('',#7422,#5800,#5801);
#4791=AXIS2_PLACEMENT_3D('',#7434,#5803,#5804);
#4792=AXIS2_PLACEMENT_3D('',#7442,#5805,#5806);
#4793=AXIS2_PLACEMENT_3D('',#7448,#5807,#5808);
#4794=AXIS2_PLACEMENT_3D('',#7455,#5809,#5810);
#4795=AXIS2_PLACEMENT_3D('',#7468,#5811,#5812);
#4796=AXIS2_PLACEMENT_3D('',#7480,#5814,#5815);
#4797=AXIS2_PLACEMENT_3D('',#7488,#5816,#5817);
#4798=AXIS2_PLACEMENT_3D('',#7494,#5818,#5819);
#4799=AXIS2_PLACEMENT_3D('',#7501,#5820,#5821);
#4800=AXIS2_PLACEMENT_3D('',#7512,#5822,#5823);
#4801=AXIS2_PLACEMENT_3D('',#7519,#5824,#5825);
#4802=AXIS2_PLACEMENT_3D('',#7530,#5826,#5827);
#4803=AXIS2_PLACEMENT_3D('',#7541,#5828,#5829);
#4804=AXIS2_PLACEMENT_3D('',#7547,#5830,#5831);
#4805=AXIS2_PLACEMENT_3D('',#7553,#5832,#5833);
#4806=AXIS2_PLACEMENT_3D('',#7554,#5834,#5835);
#4807=AXIS2_PLACEMENT_3D('',#7555,#5836,#5837);
#4808=AXIS2_PLACEMENT_3D('',#7557,#5838,#5839);
#4809=AXIS2_PLACEMENT_3D('',#7559,#5840,#5841);
#4810=AXIS2_PLACEMENT_3D('',#7560,#5842,#5843);
#4811=AXIS2_PLACEMENT_3D('',#7562,#5844,#5845);
#4812=AXIS2_PLACEMENT_3D('',#7564,#5846,#5847);
#4813=AXIS2_PLACEMENT_3D('',#7565,#5848,#5849);
#4814=AXIS2_PLACEMENT_3D('',#7571,#5850,#5851);
#4815=AXIS2_PLACEMENT_3D('',#7589,#5852,#5853);
#4816=AXIS2_PLACEMENT_3D('',#7590,#5854,#5855);
#4817=AXIS2_PLACEMENT_3D('',#7591,#5856,#5857);
#4818=AXIS2_PLACEMENT_3D('',#7592,#5858,#5859);
#4819=AXIS2_PLACEMENT_3D('',#7621,#5860,#5861);
#4820=AXIS2_PLACEMENT_3D('',#7627,#5862,#5863);
#4821=AXIS2_PLACEMENT_3D('',#7633,#5864,#5865);
#4822=AXIS2_PLACEMENT_3D('',#7634,#5866,#5867);
#4823=AXIS2_PLACEMENT_3D('',#7653,#5868,#5869);
#4824=AXIS2_PLACEMENT_3D('',#7654,#5870,#5871);
#4825=AXIS2_PLACEMENT_3D('',#7655,#5872,#5873);
#4826=AXIS2_PLACEMENT_3D('',#7671,#5874,#5875);
#4827=AXIS2_PLACEMENT_3D('',#7672,#5876,#5877);
#4828=AXIS2_PLACEMENT_3D('',#7673,#5878,#5879);
#4829=AXIS2_PLACEMENT_3D('',#7674,#5880,#5881);
#4830=AXIS2_PLACEMENT_3D('',#7675,#5882,#5883);
#4831=AXIS2_PLACEMENT_3D('',#7676,#5884,#5885);
#4832=AXIS2_PLACEMENT_3D('',#7677,#5886,#5887);
#4833=AXIS2_PLACEMENT_3D('',#7678,#5888,#5889);
#4834=AXIS2_PLACEMENT_3D('',#7700,#5890,#5891);
#4835=AXIS2_PLACEMENT_3D('',#7701,#5892,#5893);
#4836=AXIS2_PLACEMENT_3D('',#7702,#5894,#5895);
#4837=AXIS2_PLACEMENT_3D('',#7703,#5896,#5897);
#4838=AXIS2_PLACEMENT_3D('',#7719,#5898,#5899);
#4839=AXIS2_PLACEMENT_3D('',#7720,#5900,#5901);
#4840=AXIS2_PLACEMENT_3D('',#7721,#5902,#5903);
#4841=AXIS2_PLACEMENT_3D('',#7722,#5904,#5905);
#4842=AXIS2_PLACEMENT_3D('',#7723,#5906,#5907);
#4843=AXIS2_PLACEMENT_3D('',#7724,#5908,#5909);
#4844=AXIS2_PLACEMENT_3D('',#7725,#5910,#5911);
#4845=AXIS2_PLACEMENT_3D('',#7726,#5912,#5913);
#4846=AXIS2_PLACEMENT_3D('',#7748,#5914,#5915);
#4847=AXIS2_PLACEMENT_3D('',#7749,#5916,#5917);
#4848=AXIS2_PLACEMENT_3D('',#7750,#5918,#5919);
#4849=AXIS2_PLACEMENT_3D('',#7756,#5920,#5921);
#4850=AXIS2_PLACEMENT_3D('',#7774,#5922,#5923);
#4851=AXIS2_PLACEMENT_3D('',#7775,#5924,#5925);
#4852=AXIS2_PLACEMENT_3D('',#7776,#5926,#5927);
#4853=AXIS2_PLACEMENT_3D('',#7777,#5928,#5929);
#4854=AXIS2_PLACEMENT_3D('',#7806,#5930,#5931);
#4855=AXIS2_PLACEMENT_3D('',#7812,#5932,#5933);
#4856=AXIS2_PLACEMENT_3D('',#7818,#5934,#5935);
#4857=AXIS2_PLACEMENT_3D('',#7819,#5936,#5937);
#4858=AXIS2_PLACEMENT_3D('',#7838,#5938,#5939);
#4859=AXIS2_PLACEMENT_3D('',#7839,#5940,#5941);
#4860=AXIS2_PLACEMENT_3D('',#7840,#5942,#5943);
#4861=AXIS2_PLACEMENT_3D('',#7856,#5944,#5945);
#4862=AXIS2_PLACEMENT_3D('',#7857,#5946,#5947);
#4863=AXIS2_PLACEMENT_3D('',#7858,#5948,#5949);
#4864=AXIS2_PLACEMENT_3D('',#7859,#5950,#5951);
#4865=AXIS2_PLACEMENT_3D('',#7860,#5952,#5953);
#4866=AXIS2_PLACEMENT_3D('',#7861,#5954,#5955);
#4867=AXIS2_PLACEMENT_3D('',#7862,#5956,#5957);
#4868=AXIS2_PLACEMENT_3D('',#7863,#5958,#5959);
#4869=AXIS2_PLACEMENT_3D('',#7885,#5960,#5961);
#4870=AXIS2_PLACEMENT_3D('',#7886,#5962,#5963);
#4871=AXIS2_PLACEMENT_3D('',#7887,#5964,#5965);
#4872=AXIS2_PLACEMENT_3D('',#7888,#5966,#5967);
#4873=AXIS2_PLACEMENT_3D('',#7904,#5968,#5969);
#4874=AXIS2_PLACEMENT_3D('',#7905,#5970,#5971);
#4875=AXIS2_PLACEMENT_3D('',#7906,#5972,#5973);
#4876=AXIS2_PLACEMENT_3D('',#7907,#5974,#5975);
#4877=AXIS2_PLACEMENT_3D('',#7908,#5976,#5977);
#4878=AXIS2_PLACEMENT_3D('',#7909,#5978,#5979);
#4879=AXIS2_PLACEMENT_3D('',#7910,#5980,#5981);
#4880=AXIS2_PLACEMENT_3D('',#7911,#5982,#5983);
#4881=AXIS2_PLACEMENT_3D('',#7933,#5984,#5985);
#4882=AXIS2_PLACEMENT_3D('',#7934,#5986,#5987);
#4883=AXIS2_PLACEMENT_3D('',#7945,#5988,#5989);
#4884=AXIS2_PLACEMENT_3D('',#7951,#5990,#5991);
#4885=AXIS2_PLACEMENT_3D('',#7957,#5992,#5993);
#4886=AXIS2_PLACEMENT_3D('',#7958,#5994,#5995);
#4887=AXIS2_PLACEMENT_3D('',#7959,#5996,#5997);
#4888=AXIS2_PLACEMENT_3D('',#7960,#5998,#5999);
#4889=AXIS2_PLACEMENT_3D('',#7961,#6000,#6001);
#4890=AXIS2_PLACEMENT_3D('',#7962,#6002,#6003);
#4891=AXIS2_PLACEMENT_3D('',#7963,#6004,#6005);
#4892=AXIS2_PLACEMENT_3D('',#7964,#6006,#6007);
#4893=AXIS2_PLACEMENT_3D('',#7965,#6008,#6009);
#4894=AXIS2_PLACEMENT_3D('',#7966,#6010,#6011);
#4895=AXIS2_PLACEMENT_3D('',#7967,#6012,#6013);
#4896=AXIS2_PLACEMENT_3D('',#7968,#6014,#6015);
#4897=AXIS2_PLACEMENT_3D('',#7969,#6016,#6017);
#4898=AXIS2_PLACEMENT_3D('',#7970,#6018,#6019);
#4899=AXIS2_PLACEMENT_3D('',#7971,#6020,#6021);
#4900=AXIS2_PLACEMENT_3D('',#7972,#6022,#6023);
#4901=AXIS2_PLACEMENT_3D('',#7973,#6024,#6025);
#4902=AXIS2_PLACEMENT_3D('',#7974,#6026,#6027);
#4903=AXIS2_PLACEMENT_3D('',#7975,#6028,#6029);
#4904=AXIS2_PLACEMENT_3D('',#7976,#6030,#6031);
#4905=AXIS2_PLACEMENT_3D('',#7977,#6032,#6033);
#4906=AXIS2_PLACEMENT_3D('',#7978,#6034,#6035);
#4907=AXIS2_PLACEMENT_3D('',#7979,#6036,#6037);
#4908=AXIS2_PLACEMENT_3D('',#7980,#6038,#6039);
#4909=AXIS2_PLACEMENT_3D('',#7981,#6040,#6041);
#4910=AXIS2_PLACEMENT_3D('',#7982,#6042,#6043);
#4911=AXIS2_PLACEMENT_3D('',#7983,#6044,#6045);
#4912=AXIS2_PLACEMENT_3D('',#7984,#6046,#6047);
#4913=AXIS2_PLACEMENT_3D('',#7985,#6048,#6049);
#4914=AXIS2_PLACEMENT_3D('',#7986,#6050,#6051);
#4915=AXIS2_PLACEMENT_3D('',#7987,#6052,#6053);
#4916=AXIS2_PLACEMENT_3D('',#7988,#6054,#6055);
#4917=AXIS2_PLACEMENT_3D('',#7989,#6056,#6057);
#4918=AXIS2_PLACEMENT_3D('',#7994,#6058,#6059);
#4919=AXIS2_PLACEMENT_3D('',#7999,#6060,#6061);
#4920=AXIS2_PLACEMENT_3D('',#8000,#6062,#6063);
#4921=AXIS2_PLACEMENT_3D('',#8001,#6064,#6065);
#4922=AXIS2_PLACEMENT_3D('',#8002,#6066,#6067);
#4923=AXIS2_PLACEMENT_3D('',#8003,#6068,#6069);
#4924=AXIS2_PLACEMENT_3D('',#8004,#6070,#6071);
#4925=AXIS2_PLACEMENT_3D('',#8005,#6072,#6073);
#4926=AXIS2_PLACEMENT_3D('',#8006,#6074,#6075);
#4927=AXIS2_PLACEMENT_3D('',#8007,#6076,#6077);
#4928=AXIS2_PLACEMENT_3D('',#8008,#6078,#6079);
#4929=AXIS2_PLACEMENT_3D('',#8009,#6080,#6081);
#4930=AXIS2_PLACEMENT_3D('',#8010,#6082,#6083);
#4931=AXIS2_PLACEMENT_3D('',#8011,#6084,#6085);
#4932=AXIS2_PLACEMENT_3D('',#8012,#6086,#6087);
#4933=AXIS2_PLACEMENT_3D('',#8013,#6088,#6089);
#4934=AXIS2_PLACEMENT_3D('',#8014,#6090,#6091);
#4935=AXIS2_PLACEMENT_3D('',#8019,#6092,#6093);
#4936=AXIS2_PLACEMENT_3D('',#8024,#6094,#6095);
#4937=AXIS2_PLACEMENT_3D('',#8025,#6096,#6097);
#4938=AXIS2_PLACEMENT_3D('',#8026,#6098,#6099);
#4939=AXIS2_PLACEMENT_3D('',#8027,#6100,#6101);
#5064=DIRECTION('',(0.,0.,1.));
#5065=DIRECTION('',(1.,0.,0.));
#5454=DIRECTION('',(0.,1.11917643611407E-16,-1.));
#5455=DIRECTION('',(0.,1.,1.11917643611407E-16));
#5456=DIRECTION('',(0.,-1.,-1.11917643611407E-16));
#5457=DIRECTION('',(-1.,0.,0.));
#5458=DIRECTION('',(0.,1.11917643611407E-16,-1.));
#5459=DIRECTION('',(0.,1.,1.11917643611407E-16));
#5460=DIRECTION('',(-1.,0.,0.));
#5461=DIRECTION('',(0.,-1.,-1.11917643611407E-16));
#5462=DIRECTION('',(0.,1.11917643611407E-16,-1.));
#5463=DIRECTION('',(0.,1.,1.11917643611407E-16));
#5464=DIRECTION('',(0.,1.11917643611407E-16,-1.));
#5465=DIRECTION('',(0.,1.,1.11917643611407E-16));
#5466=DIRECTION('',(0.,1.11917643611407E-16,-1.));
#5467=DIRECTION('',(0.,1.,1.11917643611407E-16));
#5468=DIRECTION('',(0.,1.11917643611407E-16,-1.));
#5469=DIRECTION('',(0.,1.,1.11917643611407E-16));
#5470=DIRECTION('',(-1.,0.,0.));
#5471=DIRECTION('',(0.,-1.,-1.11917643611407E-16));
#5472=DIRECTION('',(0.,1.11917643611407E-16,-1.));
#5473=DIRECTION('',(0.,1.,1.11917643611407E-16));
#5474=DIRECTION('',(0.,1.11917643611407E-16,-1.));
#5475=DIRECTION('',(0.,1.,1.11917643611407E-16));
#5476=DIRECTION('',(0.,1.11917643611407E-16,-1.));
#5477=DIRECTION('',(0.,1.,1.11917643611407E-16));
#5478=DIRECTION('',(0.,-1.,-1.11917643611407E-16));
#5479=DIRECTION('',(-1.,0.,0.));
#5480=DIRECTION('',(0.,1.11917643611407E-16,-1.));
#5481=DIRECTION('',(0.,1.,1.11917643611407E-16));
#5482=DIRECTION('',(-1.,0.,0.));
#5483=DIRECTION('',(0.,0.,1.));
#5484=DIRECTION('',(0.,0.,1.));
#5485=DIRECTION('',(0.,-1.,-1.11917643611407E-16));
#5486=DIRECTION('',(0.,0.,-1.));
#5487=DIRECTION('',(0.,-1.,-1.11917643611407E-16));
#5488=DIRECTION('',(-1.,0.,0.));
#5489=DIRECTION('',(0.,0.,1.));
#5490=DIRECTION('',(0.,-1.,-1.11917643611407E-16));
#5491=DIRECTION('',(0.,0.,1.));
#5492=DIRECTION('',(0.,-1.,-1.11917643611407E-16));
#5493=DIRECTION('',(0.,0.,-1.));
#5494=DIRECTION('',(0.,0.,1.));
#5495=DIRECTION('',(1.,0.,0.));
#5496=DIRECTION('',(0.,0.,1.));
#5497=DIRECTION('',(0.,0.,1.));
#5498=DIRECTION('',(1.,0.,0.));
#5499=DIRECTION('',(0.,0.,1.));
#5500=DIRECTION('',(0.,0.,1.));
#5501=DIRECTION('',(1.,0.,0.));
#5502=DIRECTION('',(0.,1.,0.));
#5503=DIRECTION('',(0.,0.,1.));
#5504=DIRECTION('',(0.,-1.,0.));
#5505=DIRECTION('',(0.,0.,-1.));
#5506=DIRECTION('',(0.,1.,0.));
#5507=DIRECTION('',(0.,0.,1.));
#5508=DIRECTION('',(0.,-1.,0.));
#5509=DIRECTION('',(0.,0.,-1.));
#5510=DIRECTION('',(0.,0.,-1.));
#5511=DIRECTION('',(-1.,0.,0.));
#5512=DIRECTION('',(0.,0.,-1.));
#5513=DIRECTION('',(0.,0.,1.));
#5514=DIRECTION('',(1.,0.,0.));
#5515=DIRECTION('',(0.,0.,-1.));
#5516=DIRECTION('',(0.,1.11917643611407E-16,-1.));
#5517=DIRECTION('',(0.,1.,1.11917643611407E-16));
#5518=DIRECTION('',(0.,0.,1.));
#5519=DIRECTION('',(1.,0.,0.));
#5520=DIRECTION('',(1.,0.,0.));
#5521=DIRECTION('',(1.,0.,0.));
#5522=DIRECTION('',(0.,0.,1.));
#5523=DIRECTION('',(1.,0.,0.));
#5524=DIRECTION('',(0.,1.11917643611407E-16,-1.));
#5525=DIRECTION('',(0.,1.,1.11917643611407E-16));
#5526=DIRECTION('',(0.,0.,1.));
#5527=DIRECTION('',(0.,0.,1.));
#5528=DIRECTION('',(1.,0.,0.));
#5529=DIRECTION('',(0.,0.,1.));
#5530=DIRECTION('',(0.,0.,-1.));
#5531=DIRECTION('',(1.,0.,0.));
#5532=DIRECTION('',(-1.,0.,0.));
#5533=DIRECTION('',(-1.,0.,0.));
#5534=DIRECTION('',(0.,-1.,-1.11917643611407E-16));
#5535=DIRECTION('',(0.,1.11917643611407E-16,-1.));
#5536=DIRECTION('',(0.,-1.,0.));
#5537=DIRECTION('',(0.,0.,-1.));
#5538=DIRECTION('',(0.,-1.,0.));
#5539=DIRECTION('',(0.,0.,-1.));
#5540=DIRECTION('',(0.,1.,1.11917643611407E-16));
#5541=DIRECTION('',(0.,-1.11917643611407E-16,1.));
#5542=DIRECTION('',(0.,-1.,0.));
#5543=DIRECTION('',(0.,0.,-1.));
#5544=DIRECTION('',(0.,-1.,0.));
#5545=DIRECTION('',(0.,0.,-1.));
#5546=DIRECTION('',(0.,1.,1.11917643611407E-16));
#5547=DIRECTION('',(0.,-1.11917643611407E-16,1.));
#5548=DIRECTION('',(0.,-1.,0.));
#5549=DIRECTION('',(0.,0.,-1.));
#5550=DIRECTION('',(0.,1.,0.));
#5551=DIRECTION('',(0.,0.,1.));
#5552=DIRECTION('',(0.,-1.,-1.11917643611407E-16));
#5553=DIRECTION('',(0.,1.11917643611407E-16,-1.));
#5554=DIRECTION('',(0.,-1.,0.));
#5555=DIRECTION('',(0.,0.,-1.));
#5556=DIRECTION('',(0.,1.,0.));
#5557=DIRECTION('',(0.,0.,1.));
#5558=DIRECTION('',(0.,1.11917643611407E-16,-1.));
#5559=DIRECTION('',(0.,1.,1.11917643611407E-16));
#5560=DIRECTION('',(0.,1.11917643611407E-16,-1.));
#5561=DIRECTION('',(0.,1.,1.11917643611407E-16));
#5562=DIRECTION('',(0.,7.65524871482112E-17,-1.));
#5563=DIRECTION('',(0.,1.,7.65524871482112E-17));
#5564=DIRECTION('',(-0.0560813448397478,-0.998426202961924,-7.643200907068E-17));
#5565=DIRECTION('',(0.,7.65524871482112E-17,-1.));
#5566=DIRECTION('',(0.,1.,7.65524871482112E-17));
#5567=DIRECTION('',(0.,7.65524871482112E-17,-1.));
#5568=DIRECTION('',(0.,1.,7.65524871482112E-17));
#5569=DIRECTION('',(0.,7.65524871482112E-17,-1.));
#5570=DIRECTION('',(0.,1.,7.65524871482112E-17));
#5571=DIRECTION('',(0.0560813448397477,0.998426202961924,7.643200907068E-17));
#5572=DIRECTION('',(0.,7.65524871482112E-17,-1.));
#5573=DIRECTION('',(0.,1.,7.65524871482112E-17));
#5574=DIRECTION('',(0.,7.65524871482112E-17,-1.));
#5575=DIRECTION('',(0.,1.,7.65524871482112E-17));
#5576=DIRECTION('',(0.,7.65524871482112E-17,-1.));
#5577=DIRECTION('',(0.,1.,7.65524871482112E-17));
#5578=DIRECTION('',(0.,1.14828730722317E-16,-1.));
#5579=DIRECTION('',(0.,1.,1.14828730722317E-16));
#5580=DIRECTION('',(0.0560813448397478,-0.998426202961924,-1.1464801360602E-16));
#5581=DIRECTION('',(0.,1.14828730722317E-16,-1.));
#5582=DIRECTION('',(0.,1.,1.14828730722317E-16));
#5583=DIRECTION('',(0.,1.14828730722317E-16,-1.));
#5584=DIRECTION('',(0.,1.,1.14828730722317E-16));
#5585=DIRECTION('',(0.,1.14828730722317E-16,-1.));
#5586=DIRECTION('',(0.,1.,1.14828730722317E-16));
#5587=DIRECTION('',(-0.0560813448397477,0.998426202961924,1.1464801360602E-16));
#5588=DIRECTION('',(0.,1.14828730722317E-16,-1.));
#5589=DIRECTION('',(0.,1.,1.14828730722317E-16));
#5590=DIRECTION('',(0.,1.14828730722317E-16,-1.));
#5591=DIRECTION('',(0.,1.,1.14828730722317E-16));
#5592=DIRECTION('',(0.,1.14828730722317E-16,-1.));
#5593=DIRECTION('',(0.,1.,1.14828730722317E-16));
#5594=DIRECTION('',(0.,0.,-1.));
#5595=DIRECTION('',(-1.,0.,0.));
#5596=DIRECTION('',(0.,0.,-1.));
#5597=DIRECTION('',(-1.,0.,0.));
#5598=DIRECTION('',(0.,0.,-1.));
#5599=DIRECTION('',(-1.,0.,0.));
#5600=DIRECTION('',(-1.,0.,0.));
#5601=DIRECTION('',(0.,0.,-1.));
#5602=DIRECTION('',(-1.,0.,0.));
#5603=DIRECTION('',(0.,0.,-1.));
#5604=DIRECTION('',(-1.,0.,0.));
#5605=DIRECTION('',(0.,0.,-1.));
#5606=DIRECTION('',(-1.,0.,0.));
#5607=DIRECTION('',(0.,0.,-1.));
#5608=DIRECTION('',(-1.,0.,0.));
#5609=DIRECTION('',(0.,0.,1.));
#5610=DIRECTION('',(1.,0.,0.));
#5611=DIRECTION('',(0.,0.,1.));
#5612=DIRECTION('',(0.,0.,-1.));
#5613=DIRECTION('',(-1.,0.,0.));
#5614=DIRECTION('',(0.,1.14828730722317E-16,-1.));
#5615=DIRECTION('',(0.,1.,1.14828730722317E-16));
#5616=DIRECTION('',(0.,0.,1.));
#5617=DIRECTION('',(0.,7.65524871482112E-17,-1.));
#5618=DIRECTION('',(0.,1.,7.65524871482112E-17));
#5619=DIRECTION('',(0.,0.,-1.));
#5620=DIRECTION('',(-1.,0.,0.));
#5621=DIRECTION('',(0.,0.,1.));
#5622=DIRECTION('',(1.,0.,0.));
#5623=DIRECTION('',(0.,0.,-1.));
#5624=DIRECTION('',(-1.,0.,0.));
#5625=DIRECTION('',(0.,0.,1.));
#5626=DIRECTION('',(0.,0.,-1.));
#5627=DIRECTION('',(-1.,0.,0.));
#5628=DIRECTION('',(0.,7.65524871482112E-17,-1.));
#5629=DIRECTION('',(0.,1.,7.65524871482112E-17));
#5630=DIRECTION('',(0.,0.,1.));
#5631=DIRECTION('',(0.,1.14828730722317E-16,-1.));
#5632=DIRECTION('',(0.,1.,1.14828730722317E-16));
#5633=DIRECTION('',(0.,0.,-1.));
#5634=DIRECTION('',(-1.,0.,0.));
#5635=DIRECTION('',(0.,0.,-1.));
#5636=DIRECTION('',(-1.,0.,0.));
#5637=DIRECTION('',(0.,0.,-1.));
#5638=DIRECTION('',(-1.,0.,0.));
#5639=DIRECTION('',(-1.,0.,0.));
#5640=DIRECTION('',(0.,0.,-1.));
#5641=DIRECTION('',(-1.,0.,0.));
#5642=DIRECTION('',(0.,0.,-1.));
#5643=DIRECTION('',(-1.,0.,0.));
#5644=DIRECTION('',(0.,0.,-1.));
#5645=DIRECTION('',(-1.,0.,0.));
#5646=DIRECTION('',(0.,0.,-1.));
#5647=DIRECTION('',(-1.,0.,0.));
#5648=DIRECTION('',(0.,7.65524871482112E-17,-1.));
#5649=DIRECTION('',(0.,1.,7.65524871482112E-17));
#5650=DIRECTION('',(0.0560813448397478,-0.998426202961924,-7.643200907068E-17));
#5651=DIRECTION('',(0.,7.65524871482112E-17,-1.));
#5652=DIRECTION('',(0.,1.,7.65524871482112E-17));
#5653=DIRECTION('',(0.,7.65524871482112E-17,-1.));
#5654=DIRECTION('',(0.,1.,7.65524871482112E-17));
#5655=DIRECTION('',(0.,7.65524871482112E-17,-1.));
#5656=DIRECTION('',(0.,1.,7.65524871482112E-17));
#5657=DIRECTION('',(-0.0560813448397477,0.998426202961924,7.643200907068E-17));
#5658=DIRECTION('',(0.,7.65524871482112E-17,-1.));
#5659=DIRECTION('',(0.,1.,7.65524871482112E-17));
#5660=DIRECTION('',(0.,7.65524871482112E-17,-1.));
#5661=DIRECTION('',(0.,1.,7.65524871482112E-17));
#5662=DIRECTION('',(0.,7.65524871482112E-17,-1.));
#5663=DIRECTION('',(0.,1.,7.65524871482112E-17));
#5664=DIRECTION('',(0.,1.14828730722317E-16,-1.));
#5665=DIRECTION('',(0.,1.,1.14828730722317E-16));
#5666=DIRECTION('',(-0.0560813448397478,-0.998426202961924,-1.1464801360602E-16));
#5667=DIRECTION('',(0.,1.14828730722317E-16,-1.));
#5668=DIRECTION('',(0.,1.,1.14828730722317E-16));
#5669=DIRECTION('',(0.,1.14828730722317E-16,-1.));
#5670=DIRECTION('',(0.,1.,1.14828730722317E-16));
#5671=DIRECTION('',(0.,1.14828730722317E-16,-1.));
#5672=DIRECTION('',(0.,1.,1.14828730722317E-16));
#5673=DIRECTION('',(0.0560813448397477,0.998426202961924,1.1464801360602E-16));
#5674=DIRECTION('',(0.,1.14828730722317E-16,-1.));
#5675=DIRECTION('',(0.,1.,1.14828730722317E-16));
#5676=DIRECTION('',(0.,1.14828730722317E-16,-1.));
#5677=DIRECTION('',(0.,1.,1.14828730722317E-16));
#5678=DIRECTION('',(0.,1.14828730722317E-16,-1.));
#5679=DIRECTION('',(0.,1.,1.14828730722317E-16));
#5680=DIRECTION('',(0.,0.,1.));
#5681=DIRECTION('',(1.,0.,0.));
#5682=DIRECTION('',(0.,1.11917643611407E-16,-1.));
#5683=DIRECTION('',(0.,1.,1.11917643611407E-16));
#5684=DIRECTION('',(0.,0.,1.));
#5685=DIRECTION('',(0.,1.11917643611407E-16,-1.));
#5686=DIRECTION('',(0.,1.,1.11917643611407E-16));
#5687=DIRECTION('',(0.,7.65524871482112E-17,-1.));
#5688=DIRECTION('',(0.,1.,7.65524871482112E-17));
#5689=DIRECTION('',(0.,0.,1.));
#5690=DIRECTION('',(0.,1.14828730722317E-16,-1.));
#5691=DIRECTION('',(0.,1.,1.14828730722317E-16));
#5692=DIRECTION('',(0.,0.,1.));
#5693=DIRECTION('',(1.,0.,0.));
#5694=DIRECTION('',(0.,0.,-1.));
#5695=DIRECTION('',(-1.,0.,0.));
#5696=DIRECTION('',(0.,0.,-1.));
#5697=DIRECTION('',(-1.,0.,0.));
#5698=DIRECTION('',(0.,0.,1.));
#5699=DIRECTION('',(1.,0.,0.));
#5700=DIRECTION('',(0.,1.11917643611407E-16,-1.));
#5701=DIRECTION('',(0.,1.,1.11917643611407E-16));
#5702=DIRECTION('',(0.,0.,1.));
#5703=DIRECTION('',(0.,1.11917643611407E-16,-1.));
#5704=DIRECTION('',(0.,1.,1.11917643611407E-16));
#5705=DIRECTION('',(0.,1.14828730722317E-16,-1.));
#5706=DIRECTION('',(0.,1.,1.14828730722317E-16));
#5707=DIRECTION('',(0.,0.,1.));
#5708=DIRECTION('',(0.,7.65524871482112E-17,-1.));
#5709=DIRECTION('',(0.,1.,7.65524871482112E-17));
#5710=DIRECTION('',(-0.998426202961924,-0.0560813448397477,0.));
#5711=DIRECTION('',(0.0560813448397477,-0.998426202961924,0.));
#5712=DIRECTION('',(-0.0560813448397477,0.998426202961924,1.1464801360602E-16));
#5713=DIRECTION('',(-0.0560813448397477,0.998426202961924,7.643200907068E-17));
#5714=DIRECTION('',(-0.998426202961924,0.0560813448397477,0.));
#5715=DIRECTION('',(-0.0560813448397477,-0.998426202961924,0.));
#5716=DIRECTION('',(0.0560813448397477,0.998426202961924,1.1464801360602E-16));
#5717=DIRECTION('',(0.0560813448397477,0.998426202961924,7.643200907068E-17));
#5718=DIRECTION('',(0.,0.,1.));
#5719=DIRECTION('',(1.,0.,0.));
#5720=DIRECTION('',(0.,0.,-1.));
#5721=DIRECTION('',(-1.,0.,0.));
#5722=DIRECTION('',(0.,0.,1.));
#5723=DIRECTION('',(1.,0.,0.));
#5724=DIRECTION('',(-0.998426202961924,0.0560813448397478,0.));
#5725=DIRECTION('',(-0.0560813448397478,-0.998426202961924,0.));
#5726=DIRECTION('',(0.,0.,1.));
#5727=DIRECTION('',(-0.0560813448397478,-0.998426202961924,-7.643200907068E-17));
#5728=DIRECTION('',(0.,0.,1.));
#5729=DIRECTION('',(-0.0560813448397478,-0.998426202961924,0.));
#5730=DIRECTION('',(0.,0.,1.));
#5731=DIRECTION('',(1.,0.,0.));
#5732=DIRECTION('',(0.,7.65524871482112E-17,-1.));
#5733=DIRECTION('',(0.,1.,7.65524871482112E-17));
#5734=DIRECTION('',(0.,0.,1.));
#5735=DIRECTION('',(1.,0.,0.));
#5736=DIRECTION('',(0.,0.,1.));
#5737=DIRECTION('',(0.,7.65524871482112E-17,-1.));
#5738=DIRECTION('',(0.,1.,7.65524871482112E-17));
#5739=DIRECTION('',(-0.998426202961924,-0.0560813448397478,0.));
#5740=DIRECTION('',(0.0560813448397478,-0.998426202961924,0.));
#5741=DIRECTION('',(0.,0.,1.));
#5742=DIRECTION('',(0.0560813448397478,-0.998426202961924,-7.643200907068E-17));
#5743=DIRECTION('',(0.0560813448397478,-0.998426202961924,0.));
#5744=DIRECTION('',(0.,0.,1.));
#5745=DIRECTION('',(1.,0.,0.));
#5746=DIRECTION('',(0.,7.65524871482112E-17,-1.));
#5747=DIRECTION('',(0.,1.,7.65524871482112E-17));
#5748=DIRECTION('',(0.,7.65524871482112E-17,-1.));
#5749=DIRECTION('',(0.,1.,7.65524871482112E-17));
#5750=DIRECTION('',(0.,0.,1.));
#5751=DIRECTION('',(1.,0.,0.));
#5752=DIRECTION('',(0.,0.,1.));
#5753=DIRECTION('',(1.,0.,0.));
#5754=DIRECTION('',(0.0560813448397478,-0.998426202961924,0.));
#5755=DIRECTION('',(0.,0.,1.));
#5756=DIRECTION('',(1.,0.,0.));
#5757=DIRECTION('',(-0.0560813448397478,-0.998426202961924,0.));
#5758=DIRECTION('',(0.,0.,1.));
#5759=DIRECTION('',(1.,0.,0.));
#5760=DIRECTION('',(0.998426202961924,-0.0560813448397478,0.));
#5761=DIRECTION('',(0.0560813448397478,0.998426202961924,0.));
#5762=DIRECTION('',(0.,0.,-1.));
#5763=DIRECTION('',(-0.0560813448397478,-0.998426202961924,-1.1464801360602E-16));
#5764=DIRECTION('',(0.,0.,-1.));
#5765=DIRECTION('',(-0.0560813448397478,-0.998426202961924,0.));
#5766=DIRECTION('',(0.,0.,-1.));
#5767=DIRECTION('',(-1.,0.,0.));
#5768=DIRECTION('',(0.,0.,-1.));
#5769=DIRECTION('',(0.,1.14828730722317E-16,-1.));
#5770=DIRECTION('',(0.,1.,1.14828730722317E-16));
#5771=DIRECTION('',(0.,1.14828730722317E-16,-1.));
#5772=DIRECTION('',(0.,1.,1.14828730722317E-16));
#5773=DIRECTION('',(0.,0.,-1.));
#5774=DIRECTION('',(-1.,0.,0.));
#5775=DIRECTION('',(0.998426202961924,0.0560813448397478,0.));
#5776=DIRECTION('',(-0.0560813448397478,0.998426202961924,0.));
#5777=DIRECTION('',(0.,0.,-1.));
#5778=DIRECTION('',(0.0560813448397478,-0.998426202961924,-1.1464801360602E-16));
#5779=DIRECTION('',(0.0560813448397478,-0.998426202961924,0.));
#5780=DIRECTION('',(0.,0.,-1.));
#5781=DIRECTION('',(-1.,0.,0.));
#5782=DIRECTION('',(0.,1.14828730722317E-16,-1.));
#5783=DIRECTION('',(0.,1.,1.14828730722317E-16));
#5784=DIRECTION('',(0.,0.,-1.));
#5785=DIRECTION('',(-1.,0.,0.));
#5786=DIRECTION('',(0.,1.14828730722317E-16,-1.));
#5787=DIRECTION('',(0.,1.,1.14828730722317E-16));
#5788=DIRECTION('',(0.,0.,-1.));
#5789=DIRECTION('',(1.,0.,0.));
#5790=DIRECTION('',(0.0560813448397478,-0.998426202961924,0.));
#5791=DIRECTION('',(0.,0.,-1.));
#5792=DIRECTION('',(-1.,0.,0.));
#5793=DIRECTION('',(-0.0560813448397478,-0.998426202961924,0.));
#5794=DIRECTION('',(0.,0.,-1.));
#5795=DIRECTION('',(-1.,0.,0.));
#5796=DIRECTION('',(0.,1.14828730722317E-16,-1.));
#5797=DIRECTION('',(0.,1.,1.14828730722317E-16));
#5798=DIRECTION('',(0.,0.,-1.));
#5799=DIRECTION('',(-1.,0.,0.));
#5800=DIRECTION('',(1.,0.,0.));
#5801=DIRECTION('',(0.,0.,-1.));
#5802=DIRECTION('',(1.,0.,0.));
#5803=DIRECTION('',(0.,1.14828730722317E-16,-1.));
#5804=DIRECTION('',(0.,1.,1.14828730722317E-16));
#5805=DIRECTION('',(0.,0.,-1.));
#5806=DIRECTION('',(-1.,0.,0.));
#5807=DIRECTION('',(0.,7.65524871482112E-17,-1.));
#5808=DIRECTION('',(0.,1.,7.65524871482112E-17));
#5809=DIRECTION('',(0.,0.,1.));
#5810=DIRECTION('',(1.,0.,0.));
#5811=DIRECTION('',(-1.,0.,0.));
#5812=DIRECTION('',(0.,0.,1.));
#5813=DIRECTION('',(-1.,0.,0.));
#5814=DIRECTION('',(0.,7.65524871482112E-17,-1.));
#5815=DIRECTION('',(0.,1.,7.65524871482112E-17));
#5816=DIRECTION('',(0.,0.,1.));
#5817=DIRECTION('',(1.,0.,0.));
#5818=DIRECTION('',(0.,1.14828730722317E-16,-1.));
#5819=DIRECTION('',(0.,1.,1.14828730722317E-16));
#5820=DIRECTION('',(0.,1.11917643611407E-16,-1.));
#5821=DIRECTION('',(0.,1.,1.11917643611407E-16));
#5822=DIRECTION('',(0.,7.65524871482112E-17,-1.));
#5823=DIRECTION('',(0.,1.,7.65524871482112E-17));
#5824=DIRECTION('',(0.,-1.11917643611407E-16,1.));
#5825=DIRECTION('',(0.,-1.,-1.11917643611407E-16));
#5826=DIRECTION('',(0.,0.,1.));
#5827=DIRECTION('',(1.,0.,0.));
#5828=DIRECTION('',(-0.0560813448397478,0.998426202961924,0.));
#5829=DIRECTION('',(-0.998426202961924,-0.0560813448397478,0.));
#5830=DIRECTION('',(-0.0560813448397478,-0.998426202961924,0.));
#5831=DIRECTION('',(0.998426202961924,-0.0560813448397478,0.));
#5832=DIRECTION('',(0.,0.,1.));
#5833=DIRECTION('',(1.,0.,0.));
#5834=DIRECTION('',(0.,0.,1.));
#5835=DIRECTION('',(1.,0.,0.));
#5836=DIRECTION('',(0.,0.,1.));
#5837=DIRECTION('',(1.,0.,0.));
#5838=DIRECTION('',(0.,0.,1.));
#5839=DIRECTION('',(1.,0.,0.));
#5840=DIRECTION('',(0.,0.,-1.));
#5841=DIRECTION('',(1.,0.,0.));
#5842=DIRECTION('',(0.,0.,-1.));
#5843=DIRECTION('',(-1.,0.,0.));
#5844=DIRECTION('',(0.,0.,1.));
#5845=DIRECTION('',(1.,0.,0.));
#5846=DIRECTION('',(0.,1.14828730722317E-16,-1.));
#5847=DIRECTION('',(0.,1.,1.14828730722317E-16));
#5848=DIRECTION('',(0.983804137470403,-0.179246810560514,0.));
#5849=DIRECTION('',(0.179246810560514,0.983804137470403,0.));
#5850=DIRECTION('',(-0.0560813448397478,-0.998426202961924,-1.1464801360602E-16));
#5851=DIRECTION('',(0.998426202961924,-0.0560813448397478,0.));
#5852=DIRECTION('',(0.983804137470403,0.179246810560514,0.));
#5853=DIRECTION('',(-0.179246810560514,0.983804137470403,0.));
#5854=DIRECTION('',(0.,1.14828730722317E-16,-1.));
#5855=DIRECTION('',(0.,1.,1.14828730722317E-16));
#5856=DIRECTION('',(0.642413406945013,0.766358280817335,1.11440961830976E-15));
#5857=DIRECTION('',(-0.766358280817335,0.642413406945013,0.));
#5858=DIRECTION('',(0.,1.14828730722317E-16,-1.));
#5859=DIRECTION('',(0.,1.,1.14828730722317E-16));
#5860=DIRECTION('',(-0.0560813448397478,0.998426202961924,1.1464801360602E-16));
#5861=DIRECTION('',(-0.998426202961924,-0.0560813448397478,0.));
#5862=DIRECTION('',(0.999999999999785,6.01294052053665E-7,-2.61609735228368E-7));
#5863=DIRECTION('',(-6.01294052053685E-7,0.999999999999819,0.));
#5864=DIRECTION('',(0.,1.14828730722317E-16,-1.));
#5865=DIRECTION('',(0.,1.,1.14828730722317E-16));
#5866=DIRECTION('',(-0.642413406945014,0.766358280817334,0.));
#5867=DIRECTION('',(-0.766358280817334,-0.642413406945014,0.));
#5868=DIRECTION('',(0.,1.11917643611407E-16,-1.));
#5869=DIRECTION('',(0.,1.,1.11917643611407E-16));
#5870=DIRECTION('',(-0.552533958187431,-0.833490386897012,-9.32822800742734E-17));
#5871=DIRECTION('',(0.833490386897012,-0.552533958187431,0.));
#5872=DIRECTION('',(-0.928501017043572,-0.371329855181418,-4.15583623944693E-17));
#5873=DIRECTION('',(0.371329855181418,-0.928501017043572,0.));
#5874=DIRECTION('',(-0.535520596090342,-0.807825948455544,-0.246241605267967));
#5875=DIRECTION('',(0.833490386897012,-0.552533958187431,0.));
#5876=DIRECTION('',(0.197352473808094,0.980332597173952,0.));
#5877=DIRECTION('',(-0.980332597173952,0.197352473808094,0.));
#5878=DIRECTION('',(0.,1.14828730722317E-16,-1.));
#5879=DIRECTION('',(0.,1.,1.14828730722317E-16));
#5880=DIRECTION('',(0.0560813448397463,0.998426202961924,0.));
#5881=DIRECTION('',(-0.998426202961924,0.0560813448397463,0.));
#5882=DIRECTION('',(0.0560813448397477,0.998426202961924,1.1464801360602E-16));
#5883=DIRECTION('',(-0.998426202961924,0.0560813448397477,0.));
#5884=DIRECTION('',(0.0560813448397463,0.998426202961924,0.));
#5885=DIRECTION('',(-0.998426202961924,0.0560813448397463,0.));
#5886=DIRECTION('',(0.,1.14828730722317E-16,-1.));
#5887=DIRECTION('',(0.,1.,1.14828730722317E-16));
#5888=DIRECTION('',(-0.0527919210430931,0.998605534268952,0.));
#5889=DIRECTION('',(-0.998605534268952,-0.0527919210430931,0.));
#5890=DIRECTION('',(0.234713071091589,-0.914083668468321,0.330697477006177));
#5891=DIRECTION('',(0.,-0.340201097913941,-0.940352706689436));
#5892=DIRECTION('',(0.,1.11917643611407E-16,-1.));
#5893=DIRECTION('',(0.,1.,1.11917643611407E-16));
#5894=DIRECTION('',(-0.928501017043572,0.371329855181418,4.15583623944693E-17));
#5895=DIRECTION('',(-0.371329855181418,-0.928501017043572,0.));
#5896=DIRECTION('',(-0.552533958187431,0.833490386897012,9.32822800742734E-17));
#5897=DIRECTION('',(-0.833490386897012,-0.552533958187431,0.));
#5898=DIRECTION('',(-0.535520596090342,0.807825948455544,0.246241605267967));
#5899=DIRECTION('',(-0.833490386897012,-0.552533958187431,0.));
#5900=DIRECTION('',(-0.197352473808102,0.98033259717395,0.));
#5901=DIRECTION('',(-0.98033259717395,-0.197352473808102,0.));
#5902=DIRECTION('',(0.,1.14828730722317E-16,-1.));
#5903=DIRECTION('',(0.,1.,1.14828730722317E-16));
#5904=DIRECTION('',(-0.05608134483975,0.998426202961924,3.85312924844834E-15));
#5905=DIRECTION('',(-0.998426202961924,-0.05608134483975,0.));
#5906=DIRECTION('',(0.0560813448397477,-0.998426202961924,-1.1464801360602E-16));
#5907=DIRECTION('',(0.998426202961924,0.0560813448397477,0.));
#5908=DIRECTION('',(-0.0560813448397466,0.998426202961924,0.));
#5909=DIRECTION('',(-0.998426202961924,-0.0560813448397466,0.));
#5910=DIRECTION('',(0.,1.14828730722317E-16,-1.));
#5911=DIRECTION('',(0.,1.,1.14828730722317E-16));
#5912=DIRECTION('',(0.0527919210430855,0.998605534268953,7.6618529323497E-15));
#5913=DIRECTION('',(-0.998605534268953,0.0527919210430855,0.));
#5914=DIRECTION('',(0.234713071091591,0.914083668468322,-0.330697477006173));
#5915=DIRECTION('',(0.,0.340201097913937,0.940352706689437));
#5916=DIRECTION('',(0.,7.65524871482112E-17,-1.));
#5917=DIRECTION('',(0.,1.,7.65524871482112E-17));
#5918=DIRECTION('',(-0.9838041374704,-0.17924681056053,0.));
#5919=DIRECTION('',(0.17924681056053,-0.9838041374704,0.));
#5920=DIRECTION('',(-0.0560813448397478,0.998426202961924,7.643200907068E-17));
#5921=DIRECTION('',(-0.998426202961924,-0.0560813448397478,0.));
#5922=DIRECTION('',(-0.9838041374704,0.17924681056053,0.));
#5923=DIRECTION('',(-0.17924681056053,-0.9838041374704,0.));
#5924=DIRECTION('',(0.,7.65524871482112E-17,-1.));
#5925=DIRECTION('',(0.,1.,7.65524871482112E-17));
#5926=DIRECTION('',(-0.642413406945013,0.766358280817335,0.));
#5927=DIRECTION('',(-0.766358280817335,-0.642413406945013,0.));
#5928=DIRECTION('',(0.,7.65524871482112E-17,-1.));
#5929=DIRECTION('',(0.,1.,7.65524871482112E-17));
#5930=DIRECTION('',(-0.0560813448397478,-0.998426202961924,-7.643200907068E-17));
#5931=DIRECTION('',(0.998426202961924,-0.0560813448397478,0.));
#5932=DIRECTION('',(0.999999999999784,6.04763510871776E-7,2.58438346553984E-7));
#5933=DIRECTION('',(-6.04763510871797E-7,0.999999999999817,0.));
#5934=DIRECTION('',(0.,7.65524871482112E-17,-1.));
#5935=DIRECTION('',(0.,1.,7.65524871482112E-17));
#5936=DIRECTION('',(0.642413406945013,0.766358280817335,0.));
#5937=DIRECTION('',(-0.766358280817335,0.642413406945013,0.));
#5938=DIRECTION('',(0.,1.11917643611407E-16,-1.));
#5939=DIRECTION('',(0.,1.,1.11917643611407E-16));
#5940=DIRECTION('',(-0.552533958187431,0.833490386897012,9.32822800742734E-17));
#5941=DIRECTION('',(-0.833490386897012,-0.552533958187431,0.));
#5942=DIRECTION('',(-0.928501017043572,0.371329855181418,4.15583623944693E-17));
#5943=DIRECTION('',(-0.371329855181418,-0.928501017043572,0.));
#5944=DIRECTION('',(0.535520596090342,-0.807825948455544,0.246241605267969));
#5945=DIRECTION('',(0.833490386897012,0.552533958187431,0.));
#5946=DIRECTION('',(-0.197352473808615,0.980332597173847,-2.23319085694374E-13));
#5947=DIRECTION('',(-0.980332597173847,-0.197352473808615,0.));
#5948=DIRECTION('',(0.,7.65524871482112E-17,-1.));
#5949=DIRECTION('',(0.,1.,7.65524871482112E-17));
#5950=DIRECTION('',(-0.0560813448397463,0.998426202961924,0.));
#5951=DIRECTION('',(-0.998426202961924,-0.0560813448397463,0.));
#5952=DIRECTION('',(-0.0560813448397477,0.998426202961924,7.643200907068E-17));
#5953=DIRECTION('',(-0.998426202961924,-0.0560813448397477,0.));
#5954=DIRECTION('',(-0.0560813448397463,0.998426202961924,0.));
#5955=DIRECTION('',(-0.998426202961924,-0.0560813448397463,0.));
#5956=DIRECTION('',(0.,7.65524871482112E-17,-1.));
#5957=DIRECTION('',(0.,1.,7.65524871482112E-17));
#5958=DIRECTION('',(0.0527919210430856,0.998605534268953,0.));
#5959=DIRECTION('',(-0.998605534268953,0.0527919210430856,0.));
#5960=DIRECTION('',(-0.23471307109159,-0.914083668468321,-0.330697477006176));
#5961=DIRECTION('',(0.,0.34020109791394,-0.940352706689436));
#5962=DIRECTION('',(0.,1.11917643611407E-16,-1.));
#5963=DIRECTION('',(0.,1.,1.11917643611407E-16));
#5964=DIRECTION('',(-0.552533958187431,-0.833490386897012,-9.32822800742734E-17));
#5965=DIRECTION('',(0.833490386897012,-0.552533958187431,0.));
#5966=DIRECTION('',(-0.928501017043572,-0.371329855181418,-4.15583623944693E-17));
#5967=DIRECTION('',(0.371329855181418,-0.928501017043572,0.));
#5968=DIRECTION('',(0.535520596090342,0.807825948455544,-0.246241605267969));
#5969=DIRECTION('',(-0.833490386897011,0.552533958187431,0.));
#5970=DIRECTION('',(0.197352473808095,0.980332597173951,0.));
#5971=DIRECTION('',(-0.980332597173952,0.197352473808095,0.));
#5972=DIRECTION('',(0.,7.65524871482112E-17,-1.));
#5973=DIRECTION('',(0.,1.,7.65524871482112E-17));
#5974=DIRECTION('',(0.05608134483975,0.998426202961924,-3.85312924844833E-15));
#5975=DIRECTION('',(-0.998426202961924,0.05608134483975,0.));
#5976=DIRECTION('',(-0.0560813448397477,-0.998426202961924,-7.643200907068E-17));
#5977=DIRECTION('',(0.998426202961924,-0.0560813448397477,0.));
#5978=DIRECTION('',(0.0560813448397466,0.998426202961924,0.));
#5979=DIRECTION('',(-0.998426202961924,0.0560813448397466,0.));
#5980=DIRECTION('',(0.,7.65524871482112E-17,-1.));
#5981=DIRECTION('',(0.,1.,7.65524871482112E-17));
#5982=DIRECTION('',(-0.0527919210431341,0.99860553426895,-2.21826550717474E-13));
#5983=DIRECTION('',(-0.99860553426895,-0.0527919210431341,0.));
#5984=DIRECTION('',(-0.234713071091591,0.914083668468323,0.330697477006171));
#5985=DIRECTION('',(0.,-0.340201097913935,0.940352706689438));
#5986=DIRECTION('',(0.,0.,-1.));
#5987=DIRECTION('',(-1.,0.,0.));
#5988=DIRECTION('',(0.0560813448397478,0.998426202961924,0.));
#5989=DIRECTION('',(-0.998426202961924,0.0560813448397478,0.));
#5990=DIRECTION('',(0.0560813448397478,-0.998426202961924,0.));
#5991=DIRECTION('',(0.998426202961924,0.0560813448397478,0.));
#5992=DIRECTION('',(0.,0.,-1.));
#5993=DIRECTION('',(-1.,0.,0.));
#5994=DIRECTION('',(0.,0.,1.));
#5995=DIRECTION('',(1.,0.,0.));
#5996=DIRECTION('',(0.756219796281132,0.654317674919854,-2.62366446721458E-15));
#5997=DIRECTION('',(-0.654317674919854,0.756219796281132,0.));
#5998=DIRECTION('',(0.,-1.11917643611407E-16,1.));
#5999=DIRECTION('',(0.,-1.,-1.11917643611407E-16));
#6000=DIRECTION('',(0.756219796281135,-0.65431767491985,1.91657645850553E-15));
#6001=DIRECTION('',(0.65431767491985,0.756219796281135,0.));
#6002=DIRECTION('',(0.,0.,1.));
#6003=DIRECTION('',(1.,0.,0.));
#6004=DIRECTION('',(-1.,0.,0.));
#6005=DIRECTION('',(0.,0.,1.));
#6006=DIRECTION('',(0.,0.,1.));
#6007=DIRECTION('',(1.,0.,0.));
#6008=DIRECTION('',(0.,0.,1.));
#6009=DIRECTION('',(1.,0.,0.));
#6010=DIRECTION('',(-3.46944695195364E-15,-1.38751515677455E-15,1.));
#6011=DIRECTION('',(1.,0.,3.46944695195364E-15));
#6012=DIRECTION('',(-1.,0.,0.));
#6013=DIRECTION('',(0.,0.,1.));
#6014=DIRECTION('',(-1.,0.,0.));
#6015=DIRECTION('',(0.,0.,1.));
#6016=DIRECTION('',(0.,-1.86830541284738E-15,1.));
#6017=DIRECTION('',(0.,-1.,-1.86830541284738E-15));
#6018=DIRECTION('',(0.,0.,1.));
#6019=DIRECTION('',(1.,0.,0.));
#6020=DIRECTION('',(0.,0.,1.));
#6021=DIRECTION('',(1.,0.,0.));
#6022=DIRECTION('',(-1.,0.,0.));
#6023=DIRECTION('',(0.,0.,1.));
#6024=DIRECTION('',(0.,0.,1.));
#6025=DIRECTION('',(1.,0.,0.));
#6026=DIRECTION('',(-0.756219796281137,0.654317674919848,2.62366446721458E-15));
#6027=DIRECTION('',(-0.654317674919848,-0.756219796281137,0.));
#6028=DIRECTION('',(0.,-1.11917643611407E-16,1.));
#6029=DIRECTION('',(0.,-1.,-1.11917643611407E-16));
#6030=DIRECTION('',(-0.756219796281092,-0.6543176749199,0.));
#6031=DIRECTION('',(0.6543176749199,-0.756219796281092,0.));
#6032=DIRECTION('',(0.,0.,1.));
#6033=DIRECTION('',(1.,0.,0.));
#6034=DIRECTION('',(0.,0.,-1.));
#6035=DIRECTION('',(-1.,0.,0.));
#6036=DIRECTION('',(0.299336048990059,-0.954147750495184,0.));
#6037=DIRECTION('',(0.954147750495185,0.299336048990059,0.));
#6038=DIRECTION('',(-0.299336048990059,-0.954147750495184,0.));
#6039=DIRECTION('',(0.954147750495185,-0.299336048990059,0.));
#6040=DIRECTION('',(0.,0.,-1.));
#6041=DIRECTION('',(-1.,0.,0.));
#6042=DIRECTION('',(-0.248706066143853,-0.968579006928836,0.));
#6043=DIRECTION('',(0.968579006928836,-0.248706066143853,0.));
#6044=DIRECTION('',(0.,0.,-1.));
#6045=DIRECTION('',(-1.,0.,0.));
#6046=DIRECTION('',(0.248706066143863,-0.968579006928833,0.));
#6047=DIRECTION('',(0.968579006928833,0.248706066143863,0.));
#6048=DIRECTION('',(0.,0.,-1.));
#6049=DIRECTION('',(-1.,0.,0.));
#6050=DIRECTION('',(-0.517694816437262,-0.855565355209051,0.));
#6051=DIRECTION('',(0.855565355209051,-0.517694816437262,0.));
#6052=DIRECTION('',(0.,0.,-1.));
#6053=DIRECTION('',(-1.,0.,0.));
#6054=DIRECTION('',(0.517694816437954,-0.855565355208632,8.98057351466427E-16));
#6055=DIRECTION('',(0.855565355208632,0.517694816437955,0.));
#6056=DIRECTION('',(0.,0.,1.));
#6057=DIRECTION('',(1.,0.,0.));
#6058=DIRECTION('',(0.,0.,1.));
#6059=DIRECTION('',(1.,0.,0.));
#6060=DIRECTION('',(1.,0.,0.));
#6061=DIRECTION('',(0.,0.,-1.));
#6062=DIRECTION('',(0.,0.,-1.));
#6063=DIRECTION('',(-1.,0.,0.));
#6064=DIRECTION('',(0.,0.,-1.));
#6065=DIRECTION('',(-1.,0.,0.));
#6066=DIRECTION('',(0.,0.,1.));
#6067=DIRECTION('',(1.,0.,0.));
#6068=DIRECTION('',(0.,0.,-1.));
#6069=DIRECTION('',(-1.,0.,0.));
#6070=DIRECTION('',(0.299336048990059,-0.954147750495184,0.));
#6071=DIRECTION('',(0.954147750495185,0.299336048990059,0.));
#6072=DIRECTION('',(-0.299336048990059,-0.954147750495185,0.));
#6073=DIRECTION('',(0.954147750495185,-0.299336048990059,0.));
#6074=DIRECTION('',(0.,0.,-1.));
#6075=DIRECTION('',(-1.,0.,0.));
#6076=DIRECTION('',(-0.248706066143425,-0.968579006928946,0.));
#6077=DIRECTION('',(0.968579006928946,-0.248706066143425,0.));
#6078=DIRECTION('',(0.,0.,-1.));
#6079=DIRECTION('',(-1.,0.,0.));
#6080=DIRECTION('',(0.24870606614387,-0.968579006928831,0.));
#6081=DIRECTION('',(0.968579006928831,0.24870606614387,0.));
#6082=DIRECTION('',(0.,0.,-1.));
#6083=DIRECTION('',(-1.,0.,0.));
#6084=DIRECTION('',(-0.517694816437967,-0.855565355208624,0.));
#6085=DIRECTION('',(0.855565355208624,-0.517694816437967,0.));
#6086=DIRECTION('',(0.,0.,-1.));
#6087=DIRECTION('',(-1.,0.,0.));
#6088=DIRECTION('',(0.517694816437267,-0.855565355209048,0.));
#6089=DIRECTION('',(0.855565355209048,0.517694816437267,0.));
#6090=DIRECTION('',(0.,0.,1.));
#6091=DIRECTION('',(1.,0.,0.));
#6092=DIRECTION('',(0.,0.,1.));
#6093=DIRECTION('',(1.,0.,0.));
#6094=DIRECTION('',(-1.,0.,0.));
#6095=DIRECTION('',(0.,0.,1.));
#6096=DIRECTION('',(0.,0.,-1.));
#6097=DIRECTION('',(-1.,0.,0.));
#6098=DIRECTION('',(0.,-1.,0.));
#6099=DIRECTION('',(1.,0.,0.));
#6100=DIRECTION('',(0.,-1.,0.));
#6101=DIRECTION('',(1.,0.,0.));
#6402=CARTESIAN_POINT('',(0.,0.,0.));
#6903=CARTESIAN_POINT('',(0.03650000008,-0.0374221052,-0.0110000004));
#6904=CARTESIAN_POINT('',(0.03550000008,-0.0924221052,-0.0110000004));
#6905=CARTESIAN_POINT('',(0.03550000008,-0.0578844846861027,-0.0110000004));
#6906=CARTESIAN_POINT('',(0.03550000008,-0.0746532949430514,-0.0110000004));
#6907=CARTESIAN_POINT('',(0.03650000008,-0.0746532949430514,-0.0110000004));
#6908=CARTESIAN_POINT('',(0.0262711300553686,-0.0746532949430514,-0.0110000004));
#6909=CARTESIAN_POINT('',(0.,-0.0684221052,-0.0110000004));
#6910=CARTESIAN_POINT('',(-0.0262711300553686,-0.0746532949430514,-0.0110000004));
#6911=CARTESIAN_POINT('',(0.03650000008,-0.0746532949430514,-0.0110000004));
#6912=CARTESIAN_POINT('',(-0.03550000008,-0.0746532949430514,-0.0110000004));
#6913=CARTESIAN_POINT('',(-0.03550000008,-0.0374221052,-0.0110000004));
#6914=CARTESIAN_POINT('',(-0.03550000008,-0.0578844846861027,-0.0110000004));
#6915=CARTESIAN_POINT('',(-0.0479406149651572,-0.0267770382679513,-0.0110000004));
#6916=CARTESIAN_POINT('',(-0.0200162970866487,-0.0452885101813074,-0.0110000004));
#6917=CARTESIAN_POINT('',(0.,-0.0684221052,-0.0110000004));
#6918=CARTESIAN_POINT('',(0.0200162970866487,-0.0452885101813074,-0.0110000004));
#6919=CARTESIAN_POINT('',(0.0479406149651572,-0.0267770382679513,-0.0110000004));
#6920=CARTESIAN_POINT('',(0.03650000008,-0.0374221052,0.0110000004));
#6921=CARTESIAN_POINT('',(0.03650000008,-0.0746532949430514,0.0110000004));
#6922=CARTESIAN_POINT('',(0.03550000008,-0.0746532949430514,0.0110000004));
#6923=CARTESIAN_POINT('',(0.0262711300553686,-0.0746532949430514,0.0110000004));
#6924=CARTESIAN_POINT('',(0.03550000008,-0.0374221052,0.0110000004));
#6925=CARTESIAN_POINT('',(0.03550000008,-0.0578844846861027,0.0110000004));
#6926=CARTESIAN_POINT('',(0.0479406149651572,-0.0267770382679513,0.0110000004));
#6927=CARTESIAN_POINT('',(0.0200162970866487,-0.0452885101813074,0.0110000004));
#6928=CARTESIAN_POINT('',(0.,-0.0684221052,0.0110000004));
#6929=CARTESIAN_POINT('',(-0.0200162970866487,-0.0452885101813074,0.0110000004));
#6930=CARTESIAN_POINT('',(-0.0479406149651572,-0.0267770382679513,0.0110000004));
#6931=CARTESIAN_POINT('',(-0.03550000008,-0.0578844846861027,0.0110000004));
#6932=CARTESIAN_POINT('',(-0.03550000008,-0.0924221052,0.0110000004));
#6933=CARTESIAN_POINT('',(-0.03550000008,-0.0746532949430514,0.0110000004));
#6934=CARTESIAN_POINT('',(0.03650000008,-0.0746532949430514,0.0110000004));
#6935=CARTESIAN_POINT('',(-0.0262711300553686,-0.0746532949430514,0.0110000004));
#6936=CARTESIAN_POINT('',(0.,-0.0684221052,0.0110000004));
#6937=CARTESIAN_POINT('',(0.03650000008,0.,0.));
#6938=CARTESIAN_POINT('',(0.03650000008,-0.0746532949430514,0.));
#6939=CARTESIAN_POINT('',(0.03650000008,-0.0746532949430514,-0.0100000004));
#6940=CARTESIAN_POINT('',(0.03650000008,-0.0746532949430514,0.0100000004));
#6941=CARTESIAN_POINT('',(0.03650000008,-0.0582659958948477,-0.0100000004));
#6942=CARTESIAN_POINT('',(0.03650000008,-0.0578844846861027,-0.0100000004));
#6943=CARTESIAN_POINT('',(0.03650000008,-0.0578844846861027,0.0100000004));
#6944=CARTESIAN_POINT('',(0.03650000008,-0.0578844846861027,0.0100000004));
#6945=CARTESIAN_POINT('',(0.03650000008,-1.11917648088113E-18,0.0100000004));
#6946=CARTESIAN_POINT('',(-0.03650000008,0.,0.));
#6947=CARTESIAN_POINT('',(-0.03650000008,1.11917648088112E-18,-0.0100000004));
#6948=CARTESIAN_POINT('',(-0.03650000008,-0.0578844846861027,-0.0100000004));
#6949=CARTESIAN_POINT('',(-0.03650000008,-0.0746532949430514,-0.0100000004));
#6950=CARTESIAN_POINT('',(-0.03650000008,-0.0746532949430514,0.));
#6951=CARTESIAN_POINT('',(-0.03650000008,-0.0746532949430514,0.0100000004));
#6952=CARTESIAN_POINT('',(-0.03650000008,-0.0582659958948477,0.0100000004));
#6953=CARTESIAN_POINT('',(-0.03650000008,-0.0578844846861027,0.0100000004));
#6954=CARTESIAN_POINT('',(-0.03650000008,-0.0578844846861027,-0.0100000004));
#6955=CARTESIAN_POINT('',(0.,-0.0684221052,-0.01200000032));
#6956=CARTESIAN_POINT('',(0.0231769772486856,-0.0746532949430514,-0.01200000032));
#6957=CARTESIAN_POINT('',(0.0231769772486856,-0.0746532949430514,0.0130000004));
#6958=CARTESIAN_POINT('',(0.0231769772486856,-0.0746532949430514,-0.0130000004));
#6959=CARTESIAN_POINT('',(0.,-0.0684221052,0.0130000004));
#6960=CARTESIAN_POINT('',(-0.0231769772486856,-0.0746532949430514,0.0130000004));
#6961=CARTESIAN_POINT('',(-0.0231769772486856,-0.0746532949430514,-0.01200000032));
#6962=CARTESIAN_POINT('',(-0.0231769772486856,-0.0746532949430514,-0.0130000004));
#6963=CARTESIAN_POINT('',(0.,-0.0684221052,-0.0130000004));
#6964=CARTESIAN_POINT('',(0.03100000008,0.,0.));
#6965=CARTESIAN_POINT('',(0.0293798995199573,-0.0534809425826498,0.00430172818359));
#6966=CARTESIAN_POINT('',(0.0309881374462023,-0.0545317846725483,0.00459986185281222));
#6967=CARTESIAN_POINT('',(0.0326675511752334,-0.0554881302704746,0.00429882440516112));
#6968=CARTESIAN_POINT('',(0.0341979731548129,-0.0562441547182963,0.00334152801974006));
#6969=CARTESIAN_POINT('',(0.0352891605534319,-0.0567197587438045,0.00176416161650936));
#6970=CARTESIAN_POINT('',(0.0356378125150989,-0.0568608009129647,-0.000181591276415526));
#6971=CARTESIAN_POINT('',(0.0351390741350192,-0.0566574377320471,-0.00209014083998486));
#6972=CARTESIAN_POINT('',(0.0339352100276026,-0.0561220403071199,-0.00357295922054393));
#6973=CARTESIAN_POINT('',(0.0323479956911139,-0.0553167615665181,-0.00440742187852888));
#6974=CARTESIAN_POINT('',(0.0306663015201423,-0.0543326379667634,-0.00458696466905457));
#6975=CARTESIAN_POINT('',(0.029082531685936,-0.0532708711617687,-0.0041774832675469));
#6976=CARTESIAN_POINT('',(0.027722072208117,-0.0522417406979562,-0.0032332420396007));
#6977=CARTESIAN_POINT('',(0.0267179667732945,-0.0514002809467995,-0.00175955242131977));
#6978=CARTESIAN_POINT('',(0.0263582399151791,-0.0510791744710138,0.000191439326551355));
#6979=CARTESIAN_POINT('',(0.0268710273639056,-0.0515336505560397,0.00208237089075824));
#6980=CARTESIAN_POINT('',(0.0279584485193938,-0.0524292452239578,0.0034539923091798));
#6981=CARTESIAN_POINT('',(0.0293798995199573,-0.0534809425826498,0.00430172818359));
#6982=CARTESIAN_POINT('',(0.0309881374462023,-0.0545317846725483,0.00459986185281222));
#6983=CARTESIAN_POINT('',(0.0326675511752334,-0.0554881302704746,0.00429882440516112));
#6984=CARTESIAN_POINT('',(0.03100000008,-0.0545160352572196,0.0045));
#6985=CARTESIAN_POINT('',(0.03100000008,-0.0746532949430514,0.));
#6986=CARTESIAN_POINT('',(0.03100000008,-0.0746532949430514,-0.0045));
#6987=CARTESIAN_POINT('',(-0.03100000008,0.,0.));
#6988=CARTESIAN_POINT('',(-0.0293798995199573,-0.0534809425826498,0.00430172818359));
#6989=CARTESIAN_POINT('',(-0.0309881374462023,-0.0545317846725483,0.00459986185281222));
#6990=CARTESIAN_POINT('',(-0.0326675511752334,-0.0554881302704746,0.00429882440516112));
#6991=CARTESIAN_POINT('',(-0.0341979731548129,-0.0562441547182964,0.00334152801974006));
#6992=CARTESIAN_POINT('',(-0.0352891605534319,-0.0567197587438045,0.00176416161650936));
#6993=CARTESIAN_POINT('',(-0.0356378125150989,-0.0568608009129647,-0.000181591276415529));
#6994=CARTESIAN_POINT('',(-0.0351390741350192,-0.0566574377320471,-0.00209014083998489));
#6995=CARTESIAN_POINT('',(-0.0339352100276026,-0.0561220403071199,-0.00357295922054392));
#6996=CARTESIAN_POINT('',(-0.0323479956911138,-0.0553167615665181,-0.00440742187852889));
#6997=CARTESIAN_POINT('',(-0.0306663015201423,-0.0543326379667634,-0.00458696466905456));
#6998=CARTESIAN_POINT('',(-0.029082531685936,-0.0532708711617687,-0.00417748326754691));
#6999=CARTESIAN_POINT('',(-0.0277220722081169,-0.0522417406979561,-0.00323324203960068));
#7000=CARTESIAN_POINT('',(-0.0267179667732945,-0.0514002809467995,-0.00175955242131978));
#7001=CARTESIAN_POINT('',(-0.0263582399151791,-0.0510791744710138,0.000191439326551348));
#7002=CARTESIAN_POINT('',(-0.0268710273639056,-0.0515336505560397,0.00208237089075823));
#7003=CARTESIAN_POINT('',(-0.0279584485193938,-0.0524292452239578,0.00345399230917982));
#7004=CARTESIAN_POINT('',(-0.0293798995199573,-0.0534809425826498,0.00430172818359));
#7005=CARTESIAN_POINT('',(-0.0309881374462023,-0.0545317846725483,0.00459986185281222));
#7006=CARTESIAN_POINT('',(-0.0326675511752334,-0.0554881302704746,0.00429882440516112));
#7007=CARTESIAN_POINT('',(-0.03100000008,-0.0545160352572196,0.0045));
#7008=CARTESIAN_POINT('',(-0.03100000008,-0.0746532949430514,0.));
#7009=CARTESIAN_POINT('',(-0.03100000008,-0.0746532949430514,-0.0045));
#7010=CARTESIAN_POINT('',(0.,-0.0684221052,0.0130000004));
#7011=CARTESIAN_POINT('',(-0.0252422715773777,-0.0746532949430514,0.0130000004));
#7012=CARTESIAN_POINT('',(-0.0252422715773777,-0.0746532949430514,0.0130000004));
#7013=CARTESIAN_POINT('',(-0.0252422715773777,-0.0746532949430514,0.0120000004));
#7014=CARTESIAN_POINT('',(0.,-0.0684221052,0.0130000004));
#7015=CARTESIAN_POINT('',(0.0252422715773777,-0.0746532949430514,0.0130000004));
#7016=CARTESIAN_POINT('',(0.0252422715773777,-0.0746532949430514,0.0130000004));
#7017=CARTESIAN_POINT('',(0.0252422715773777,-0.0746532949430514,0.0120000004));
#7018=CARTESIAN_POINT('',(0.,-0.0684221052,0.0120000004));
#7019=CARTESIAN_POINT('',(0.,0.,0.0130000004));
#7020=CARTESIAN_POINT('',(0.,-0.0746532949430514,0.0130000004));
#7021=CARTESIAN_POINT('',(0.,-0.0746532949430514,0.0130000004));
#7022=CARTESIAN_POINT('',(0.,-0.0684221052,-0.0130000004));
#7023=CARTESIAN_POINT('',(0.,-0.0684221052,-0.0120000004));
#7024=CARTESIAN_POINT('',(-0.0252422715773652,-0.0746532949430514,-0.0120000004000012));
#7025=CARTESIAN_POINT('',(0.0252422715773777,-0.0746532949430514,-0.0120000004));
#7026=CARTESIAN_POINT('',(0.0252422715773777,-0.0746532949430514,-0.0130000004));
#7027=CARTESIAN_POINT('',(0.0252422715773777,-0.0746532949430514,-0.0130000004));
#7028=CARTESIAN_POINT('',(0.,-0.0684221052,-0.0130000004));
#7029=CARTESIAN_POINT('',(-0.0252422715773777,-0.0746532949430514,-0.0130000004));
#7030=CARTESIAN_POINT('',(-0.0252422715773777,-0.0746532949430514,-0.0130000004));
#7031=CARTESIAN_POINT('',(0.,0.,-0.0130000004));
#7032=CARTESIAN_POINT('',(0.,-0.0746532949430514,-0.0130000004));
#7033=CARTESIAN_POINT('',(0.,-0.0746532949430514,-0.0130000004));
#7034=CARTESIAN_POINT('',(-0.03550000008,1.11917648088112E-18,-0.0100000004));
#7035=CARTESIAN_POINT('',(-0.03550000008,-0.0746532949430514,-0.0100000004));
#7036=CARTESIAN_POINT('',(-0.03550000008,-0.0578844846861027,-0.0100000004));
#7037=CARTESIAN_POINT('',(-0.03550000008,-0.0374221052,0.0100000004));
#7038=CARTESIAN_POINT('',(-0.03550000008,-0.0746532949430514,0.0100000004));
#7039=CARTESIAN_POINT('',(-0.03550000008,-0.0578844846861027,0.0100000004));
#7040=CARTESIAN_POINT('',(0.03550000008,-0.0374221052,-0.0100000004));
#7041=CARTESIAN_POINT('',(0.03550000008,-0.0746532949430514,-0.0100000004));
#7042=CARTESIAN_POINT('',(0.03550000008,-0.0578844846861027,-0.0100000004));
#7043=CARTESIAN_POINT('',(0.03550000008,-1.11917648088113E-18,0.0100000004));
#7044=CARTESIAN_POINT('',(0.03550000008,-0.0746532949430514,0.0100000004));
#7045=CARTESIAN_POINT('',(0.03550000008,-0.0578844846861027,0.0100000004));
#7046=CARTESIAN_POINT('',(0.,-0.0684221052,0.0120000004));
#7047=CARTESIAN_POINT('',(-0.0252422715773777,-0.0746532949430514,0.0120000004));
#7048=CARTESIAN_POINT('',(-0.0252422715773777,-0.0746532949430514,0.0117340892011008));
#7049=CARTESIAN_POINT('',(-0.0254741318712697,-0.0746532949430514,0.0112081301589468));
#7050=CARTESIAN_POINT('',(-0.0260068950976863,-0.0746532949430514,0.0110000004));
#7051=CARTESIAN_POINT('',(-0.0262711300553686,-0.0746532949430514,0.0110000004));
#7052=CARTESIAN_POINT('',(0.0262711300553686,-0.0746532949430514,0.0110000004));
#7053=CARTESIAN_POINT('',(0.0260068432764003,-0.0746532949430514,0.0110000004));
#7054=CARTESIAN_POINT('',(0.0254746601402995,-0.0746532949430514,0.0112068289794583));
#7055=CARTESIAN_POINT('',(0.0252422715773777,-0.0746532949430514,0.0117357303784197));
#7056=CARTESIAN_POINT('',(0.0252422715773777,-0.0746532949430514,0.0120000004));
#7057=CARTESIAN_POINT('',(0.,-0.0684221052,-0.0120000004));
#7058=CARTESIAN_POINT('',(-0.0262711300553686,-0.0746532949430514,-0.0110000004));
#7059=CARTESIAN_POINT('',(-0.0260041493105401,-0.0746532949430514,-0.0110000004));
#7060=CARTESIAN_POINT('',(-0.025474372265217,-0.0746532949430514,-0.0112087042075995));
#7061=CARTESIAN_POINT('',(-0.0252422715773772,-0.0746532949430514,-0.0117351103746127));
#7062=CARTESIAN_POINT('',(-0.0252422715773777,-0.0746532949430514,-0.0120000004000019));
#7063=CARTESIAN_POINT('',(0.0252422715773777,-0.0746532949430514,-0.0120000004));
#7064=CARTESIAN_POINT('',(0.0252422715773777,-0.0746532949430514,-0.0117324512139406));
#7065=CARTESIAN_POINT('',(0.0254742124828446,-0.0746532949430514,-0.0112095401021891));
#7066=CARTESIAN_POINT('',(0.0260054993852186,-0.0746532949430514,-0.0110000004));
#7067=CARTESIAN_POINT('',(0.0262711300553686,-0.0746532949430514,-0.0110000004));
#7068=CARTESIAN_POINT('',(0.03650000008,0.0532202,0.00799377303329589));
#7069=CARTESIAN_POINT('',(-0.00834780990288846,0.055739290033391,0.00799377303329589));
#7070=CARTESIAN_POINT('',(-0.0124910159490172,-0.0180229475260996,0.00799377303329588));
#7071=CARTESIAN_POINT('',(-0.00920784674600966,0.0404279004413879,0.00799377303329589));
#7072=CARTESIAN_POINT('',(0.,0.0403990320215515,0.00799377303329589));
#7073=CARTESIAN_POINT('',(-0.0070565442830717,0.0463143052920532,0.00799377303329589));
#7074=CARTESIAN_POINT('',(0.,0.06842,0.00799377303329589));
#7075=CARTESIAN_POINT('',(-0.0105921890504187,0.0477738844607493,0.00799377303329589));
#7076=CARTESIAN_POINT('',(-0.0770011542117716,0.0442631319913884,0.00799377303329589));
#7077=CARTESIAN_POINT('',(-0.0106041148871086,0.0405336272491669,0.00799377303329589));
#7078=CARTESIAN_POINT('',(-0.0144904743180211,-0.028655924125519,0.00799377303329588));
#7079=CARTESIAN_POINT('',(-0.0144904743180211,-0.028655924125519,0.00799377303329588));
#7080=CARTESIAN_POINT('',(-0.0479406149651572,-0.0267770382679513,0.00799377303329588));
#7081=CARTESIAN_POINT('',(-0.0150966619928097,-0.0333889120212214,0.00799377303329588));
#7082=CARTESIAN_POINT('',(0.,-0.0684221052,0.00799377303329588));
#7083=CARTESIAN_POINT('',(-0.00223898065795594,-0.0303403406237614,0.00799377303329588));
#7084=CARTESIAN_POINT('',(0.,-0.0180515951329767,0.00799377303329588));
#7085=CARTESIAN_POINT('',(0.03650000008,0.0532202,-0.0079937730332959));
#7086=CARTESIAN_POINT('',(0.00920631820296192,0.0404551133663912,-0.0079937730332959));
#7087=CARTESIAN_POINT('',(0.0124910159490172,-0.0180229475260996,-0.00799377303329591));
#7088=CARTESIAN_POINT('',(0.00920784674600966,0.0404279004413879,-0.0079937730332959));
#7089=CARTESIAN_POINT('',(0.,0.0403990320215515,-0.0079937730332959));
#7090=CARTESIAN_POINT('',(0.0070565442830717,0.0463143052920532,-0.0079937730332959));
#7091=CARTESIAN_POINT('',(0.,0.06842,-0.0079937730332959));
#7092=CARTESIAN_POINT('',(0.0105921890504172,0.0477738844607486,-0.0079937730332959));
#7093=CARTESIAN_POINT('',(0.0770011542117716,0.0442631319913884,-0.0079937730332959));
#7094=CARTESIAN_POINT('',(0.0106041148871086,0.0405336272491669,-0.0079937730332959));
#7095=CARTESIAN_POINT('',(0.0144904743180211,-0.028655924125519,-0.00799377303329591));
#7096=CARTESIAN_POINT('',(0.0144904743180211,-0.028655924125519,-0.00799377303329591));
#7097=CARTESIAN_POINT('',(0.0479406149651572,-0.0267770382679513,-0.00799377303329591));
#7098=CARTESIAN_POINT('',(0.0150966619928098,-0.0333889120212215,-0.00799377303329591));
#7099=CARTESIAN_POINT('',(0.,-0.0684221052,-0.00799377303329592));
#7100=CARTESIAN_POINT('',(0.00223898065795575,-0.0303403406237615,-0.00799377303329591));
#7101=CARTESIAN_POINT('',(0.,-0.0180515951329767,-0.00799377303329591));
#7102=CARTESIAN_POINT('',(0.03650000008,0.0836198,-0.01200000032));
#7103=CARTESIAN_POINT('',(0.0770011542117716,0.0442631319913884,-0.01200000032));
#7104=CARTESIAN_POINT('',(0.0135487072274815,0.0641694879715509,-0.01200000032));
#7105=CARTESIAN_POINT('',(0.0125890041486895,0.0608025080665035,-0.01200000032));
#7106=CARTESIAN_POINT('',(0.,0.06842,-0.01200000032));
#7107=CARTESIAN_POINT('',(7.67180601914802E-5,0.0537059481055745,-0.01200000032));
#7108=CARTESIAN_POINT('',(-7.79740982756669E-5,0.0537059481055745,-0.01200000032));
#7109=CARTESIAN_POINT('',(-7.67180601914596E-5,0.0537059481055745,-0.01200000032));
#7110=CARTESIAN_POINT('',(0.,0.06842,-0.01200000032));
#7111=CARTESIAN_POINT('',(-0.0125890041486895,0.0608025080665034,-0.01200000032));
#7112=CARTESIAN_POINT('',(-0.0770011542117716,0.0442631319913884,-0.01200000032));
#7113=CARTESIAN_POINT('',(-0.0135487072274815,0.0641694879715509,-0.01200000032));
#7114=CARTESIAN_POINT('',(0.,0.06842,-0.01200000032));
#7115=CARTESIAN_POINT('',(0.,0.06842,-0.01200000032));
#7116=CARTESIAN_POINT('',(-0.0132,0.06842,-0.01200000032));
#7117=CARTESIAN_POINT('',(-0.0770011542117716,0.0442631319913884,-0.01200000032));
#7118=CARTESIAN_POINT('',(-0.0145028549779767,0.0638701519225609,-0.01200000032));
#7119=CARTESIAN_POINT('',(-0.0145028549779767,0.0638701519225609,-0.01100000032));
#7120=CARTESIAN_POINT('',(-0.0145028549779767,0.0638701519225609,0.01100000032));
#7121=CARTESIAN_POINT('',(-0.0770011542117716,0.0442631319913884,-0.01100000032));
#7122=CARTESIAN_POINT('',(-0.0135575831556183,0.0605538020003595,-0.01100000032));
#7123=CARTESIAN_POINT('',(-0.0135575831556183,0.0605538020003595,-0.0110000003199999));
#7124=CARTESIAN_POINT('',(-0.0132893606164165,0.059509216620179,-0.010616320417549));
#7125=CARTESIAN_POINT('',(-0.0128216806843899,0.0574792137206106,-0.00966529500091684));
#7126=CARTESIAN_POINT('',(-0.0122598045310854,0.0543864981658248,-0.00828932161082693));
#7127=CARTESIAN_POINT('',(-0.0118307350725021,0.0511196604769446,-0.00726764709369388));
#7128=CARTESIAN_POINT('',(-0.0116516459867705,0.0488721502335481,-0.0069937730332959));
#7129=CARTESIAN_POINT('',(-0.0115907945846862,0.0477210925397055,-0.0069937730332959));
#7130=CARTESIAN_POINT('',(-0.0115907945846862,0.0477210925397055,-0.0069937730332959));
#7131=CARTESIAN_POINT('',(-0.0770011542117716,0.0442631319913884,-0.0069937730332959));
#7132=CARTESIAN_POINT('',(-0.0116025410900705,0.0405897085940067,-0.0069937730332959));
#7133=CARTESIAN_POINT('',(-0.0116025410900705,0.0405897085940067,-0.01200000032));
#7134=CARTESIAN_POINT('',(-0.0116025410900705,0.0405897085940067,0.00699377303329589));
#7135=CARTESIAN_POINT('',(-0.0770011542117716,0.0442631319913884,0.00699377303329589));
#7136=CARTESIAN_POINT('',(-0.0115907945846863,0.0477210925397086,0.00699377303329589));
#7137=CARTESIAN_POINT('',(-0.0115907945846864,0.0477210925397086,0.00699377303329589));
#7138=CARTESIAN_POINT('',(-0.0116516459867707,0.048872150233551,0.00699377303329614));
#7139=CARTESIAN_POINT('',(-0.0118307350725023,0.0511196604769469,0.00726764709369443));
#7140=CARTESIAN_POINT('',(-0.0122598045310857,0.0543864981658262,0.00828932161082755));
#7141=CARTESIAN_POINT('',(-0.01282168068439,0.0574792137206114,0.00966529500091711));
#7142=CARTESIAN_POINT('',(-0.0132893606164165,0.0595092166201793,0.0106163204175492));
#7143=CARTESIAN_POINT('',(-0.0135575831556184,0.0605538020003596,0.01100000032));
#7144=CARTESIAN_POINT('',(-0.0135575831556183,0.0605538020003596,0.01100000032));
#7145=CARTESIAN_POINT('',(-0.0770011542117716,0.0442631319913884,0.01100000032));
#7146=CARTESIAN_POINT('',(0.0770011542117716,0.0442631319913884,-0.01200000032));
#7147=CARTESIAN_POINT('',(0.0115907945846862,0.0477210925397055,-0.0069937730332959));
#7148=CARTESIAN_POINT('',(0.0116516459867705,0.0488721502335482,-0.0069937730332959));
#7149=CARTESIAN_POINT('',(0.0118307350725021,0.0511196604769446,-0.00726764709369388));
#7150=CARTESIAN_POINT('',(0.0122598045310854,0.0543864981658248,-0.00828932161082697));
#7151=CARTESIAN_POINT('',(0.0128216806843899,0.0574792137206107,-0.00966529500091678));
#7152=CARTESIAN_POINT('',(0.0132893606164165,0.0595092166201791,-0.0106163204175491));
#7153=CARTESIAN_POINT('',(0.0135575831556184,0.0605538020003596,-0.01100000032));
#7154=CARTESIAN_POINT('',(0.0115907945846862,0.0477210925397055,-0.0069937730332959));
#7155=CARTESIAN_POINT('',(0.0135575831556183,0.0605538020003596,-0.01100000032));
#7156=CARTESIAN_POINT('',(0.0770011542117716,0.0442631319913884,-0.01100000032));
#7157=CARTESIAN_POINT('',(0.0145028549779767,0.0638701519225609,-0.01100000032));
#7158=CARTESIAN_POINT('',(0.0145028549779767,0.0638701519225609,-0.01200000032));
#7159=CARTESIAN_POINT('',(0.0145028549779767,0.0638701519225609,0.01100000032));
#7160=CARTESIAN_POINT('',(0.0770011542117716,0.0442631319913884,0.01100000032));
#7161=CARTESIAN_POINT('',(0.0135575831556183,0.0605538020003596,0.01100000032));
#7162=CARTESIAN_POINT('',(0.0135575831556184,0.0605538020003596,0.01100000032));
#7163=CARTESIAN_POINT('',(0.0132893606164165,0.0595092166201791,0.0106163204175491));
#7164=CARTESIAN_POINT('',(0.0128216806843899,0.0574792137206106,0.00966529500091686));
#7165=CARTESIAN_POINT('',(0.0122598045310854,0.0543864981658248,0.00828932161082694));
#7166=CARTESIAN_POINT('',(0.0118307350725021,0.0511196604769446,0.00726764709369388));
#7167=CARTESIAN_POINT('',(0.0116516459867705,0.0488721502335482,0.00699377303329589));
#7168=CARTESIAN_POINT('',(0.0115907945846862,0.0477210925397055,0.00699377303329589));
#7169=CARTESIAN_POINT('',(0.0115907945846862,0.0477210925397055,0.00699377303329589));
#7170=CARTESIAN_POINT('',(0.0770011542117716,0.0442631319913884,0.00699377303329589));
#7171=CARTESIAN_POINT('',(0.0116025410900705,0.0405897085940067,0.00699377303329589));
#7172=CARTESIAN_POINT('',(0.0116025410900705,0.0405897085940067,-0.01200000032));
#7173=CARTESIAN_POINT('',(0.0116025410900705,0.0405897085940067,-0.0069937730332959));
#7174=CARTESIAN_POINT('',(0.0770011542117716,0.0442631319913884,-0.0069937730332959));
#7175=CARTESIAN_POINT('',(0.03650000008,0.0836198,0.01200000032));
#7176=CARTESIAN_POINT('',(-0.0770011542117716,0.0442631319913884,0.01200000032));
#7177=CARTESIAN_POINT('',(-0.0135487072274815,0.0641694879715509,0.01200000032));
#7178=CARTESIAN_POINT('',(-0.0125890041486895,0.0608025080665035,0.01200000032));
#7179=CARTESIAN_POINT('',(0.,0.06842,0.01200000032));
#7180=CARTESIAN_POINT('',(-7.67180601910061E-5,0.0537059481055745,0.01200000032));
#7181=CARTESIAN_POINT('',(0.03650000008,0.0537059481055745,0.01200000032));
#7182=CARTESIAN_POINT('',(7.67180601909946E-5,0.0537059481055745,0.01200000032));
#7183=CARTESIAN_POINT('',(0.,0.06842,0.01200000032));
#7184=CARTESIAN_POINT('',(0.0125890041486895,0.0608025080665034,0.01200000032));
#7185=CARTESIAN_POINT('',(0.0770011542117716,0.0442631319913884,0.01200000032));
#7186=CARTESIAN_POINT('',(0.0135487072274815,0.0641694879715509,0.01200000032));
#7187=CARTESIAN_POINT('',(0.,0.06842,0.01200000032));
#7188=CARTESIAN_POINT('',(0.,0.06842,0.01200000032));
#7189=CARTESIAN_POINT('',(-0.0132,0.06842,0.01200000032));
#7190=CARTESIAN_POINT('',(0.03650000008,0.0532202,0.00799377303329589));
#7191=CARTESIAN_POINT('',(0.0124894750029619,-0.017995513788137,0.00799377303329588));
#7192=CARTESIAN_POINT('',(0.00920784674600963,0.040427900441388,0.00799377303329589));
#7193=CARTESIAN_POINT('',(0.0124910159490172,-0.0180229475260995,0.00799377303329588));
#7194=CARTESIAN_POINT('',(0.,-0.0180515951329767,0.00799377303329588));
#7195=CARTESIAN_POINT('',(0.00223898065795594,-0.0303403406237614,0.00799377303329588));
#7196=CARTESIAN_POINT('',(0.,-0.0684221052,0.00799377303329588));
#7197=CARTESIAN_POINT('',(0.0150966619928115,-0.0333889120212222,0.00799377303329588));
#7198=CARTESIAN_POINT('',(0.0479406149651572,-0.0267770382679513,0.00799377303329588));
#7199=CARTESIAN_POINT('',(0.0144904743180211,-0.028655924125519,0.00799377303329588));
#7200=CARTESIAN_POINT('',(0.00997520014598791,0.0517303087616774,0.00799377303329589));
#7201=CARTESIAN_POINT('',(0.0106041148871086,0.0405336272491669,0.00799377303329589));
#7202=CARTESIAN_POINT('',(0.0770011542117716,0.0442631319913884,0.00799377303329589));
#7203=CARTESIAN_POINT('',(0.0105921890504172,0.0477738844607486,0.00799377303329589));
#7204=CARTESIAN_POINT('',(0.,0.06842,0.00799377303329589));
#7205=CARTESIAN_POINT('',(0.0070565442830717,0.0463143052920532,0.00799377303329589));
#7206=CARTESIAN_POINT('',(0.,0.0403990320215515,0.00799377303329589));
#7207=CARTESIAN_POINT('',(0.03650000008,0.0532202,-0.0079937730332959));
#7208=CARTESIAN_POINT('',(-0.00834780990288846,0.055739290033391,-0.0079937730332959));
#7209=CARTESIAN_POINT('',(-0.00920784674600963,0.0404279004413879,-0.0079937730332959));
#7210=CARTESIAN_POINT('',(-0.0124910159490172,-0.0180229475260996,-0.00799377303329591));
#7211=CARTESIAN_POINT('',(0.,-0.0180515951329767,-0.00799377303329591));
#7212=CARTESIAN_POINT('',(-0.00223898065795575,-0.0303403406237615,-0.00799377303329591));
#7213=CARTESIAN_POINT('',(0.,-0.0684221052,-0.00799377303329592));
#7214=CARTESIAN_POINT('',(-0.0150966619928098,-0.0333889120212215,-0.00799377303329591));
#7215=CARTESIAN_POINT('',(-0.0479406149651572,-0.0267770382679513,-0.00799377303329591));
#7216=CARTESIAN_POINT('',(-0.0144904743180211,-0.028655924125519,-0.00799377303329591));
#7217=CARTESIAN_POINT('',(-0.00974560658703515,0.0558178039161666,-0.0079937730332959));
#7218=CARTESIAN_POINT('',(-0.0106041148871086,0.0405336272491669,-0.0079937730332959));
#7219=CARTESIAN_POINT('',(-0.0770011542117716,0.0442631319913884,-0.0079937730332959));
#7220=CARTESIAN_POINT('',(-0.0105921890504172,0.0477738844607486,-0.0079937730332959));
#7221=CARTESIAN_POINT('',(0.,0.06842,-0.0079937730332959));
#7222=CARTESIAN_POINT('',(-0.0070565442830717,0.0463143052920532,-0.0079937730332959));
#7223=CARTESIAN_POINT('',(0.,0.0403990320215515,-0.0079937730332959));
#7224=CARTESIAN_POINT('',(-0.0479406149651572,-0.0267770382679513,-0.01200000032));
#7225=CARTESIAN_POINT('',(-0.0479406149651572,-0.0267770382679513,-0.0100000004));
#7226=CARTESIAN_POINT('',(-0.0208497874735458,-0.0447359762231199,-0.0100000004));
#7227=CARTESIAN_POINT('',(-0.0358713299351814,-0.0569559836690592,-0.0100000004));
#7228=CARTESIAN_POINT('',(-0.0358713299351814,-0.0569559836690592,-0.01200000032));
#7229=CARTESIAN_POINT('',(-0.0358713299351814,-0.0569559836690592,0.0100000004));
#7230=CARTESIAN_POINT('',(-0.0479406149651572,-0.0267770382679513,0.0100000004));
#7231=CARTESIAN_POINT('',(-0.0208497874735458,-0.0447359762231199,0.0100000004));
#7232=CARTESIAN_POINT('',(-0.0208497874735458,-0.0447359762231199,0.0100000004));
#7233=CARTESIAN_POINT('',(-0.0196876809355329,-0.0429829534203924,0.00944920348110594));
#7234=CARTESIAN_POINT('',(-0.0177795515520167,-0.039402141360841,0.00790667524421345));
#7235=CARTESIAN_POINT('',(-0.0165079106461819,-0.0353321005215666,0.00699377303329588));
#7236=CARTESIAN_POINT('',(-0.0160769945899836,-0.0331915595474134,0.00699377303329588));
#7237=CARTESIAN_POINT('',(-0.0160769945899836,-0.0331915595474134,0.00699377303329588));
#7238=CARTESIAN_POINT('',(-0.0479406149651572,-0.0267770382679513,0.00699377303329588));
#7239=CARTESIAN_POINT('',(-0.015488900520983,-0.0285998427806792,0.00699377303329588));
#7240=CARTESIAN_POINT('',(-0.015488900520983,-0.0285998427806792,-0.01200000032));
#7241=CARTESIAN_POINT('',(-0.015488900520983,-0.0285998427806792,-0.00699377303329591));
#7242=CARTESIAN_POINT('',(-0.0479406149651572,-0.0267770382679513,-0.00699377303329591));
#7243=CARTESIAN_POINT('',(-0.0160769945899837,-0.0331915595474134,-0.00699377303329591));
#7244=CARTESIAN_POINT('',(-0.0160769945899837,-0.0331915595474134,-0.00699377303329591));
#7245=CARTESIAN_POINT('',(-0.0165079106461819,-0.0353321005215667,-0.00699377303329591));
#7246=CARTESIAN_POINT('',(-0.0177795515520167,-0.0394021413608411,-0.00790667524421339));
#7247=CARTESIAN_POINT('',(-0.0196876809355329,-0.0429829534203924,-0.00944920348110595));
#7248=CARTESIAN_POINT('',(-0.0208497874735458,-0.0447359762231199,-0.0100000004));
#7249=CARTESIAN_POINT('',(0.,0.06842,-0.01200000032));
#7250=CARTESIAN_POINT('',(0.,0.06842,-0.01100000032));
#7251=CARTESIAN_POINT('',(0.,0.06842,0.01100000032));
#7252=CARTESIAN_POINT('',(0.0479406149651572,-0.0267770382679513,-0.01200000032));
#7253=CARTESIAN_POINT('',(0.0479406149651572,-0.0267770382679513,0.0100000004));
#7254=CARTESIAN_POINT('',(0.0208497874735458,-0.0447359762231199,0.0100000004));
#7255=CARTESIAN_POINT('',(0.0358713299351814,-0.0569559836690592,0.0100000004));
#7256=CARTESIAN_POINT('',(0.0358713299351814,-0.0569559836690592,-0.01200000032));
#7257=CARTESIAN_POINT('',(0.0358713299351814,-0.0569559836690592,-0.0100000004));
#7258=CARTESIAN_POINT('',(0.0479406149651572,-0.0267770382679513,-0.0100000004));
#7259=CARTESIAN_POINT('',(0.0208497874735458,-0.0447359762231199,-0.0100000004));
#7260=CARTESIAN_POINT('',(0.0208497874735458,-0.0447359762231199,-0.0100000004));
#7261=CARTESIAN_POINT('',(0.0196876809355329,-0.0429829534203924,-0.00944920348110595));
#7262=CARTESIAN_POINT('',(0.0177795515520167,-0.0394021413608411,-0.0079066752442134));
#7263=CARTESIAN_POINT('',(0.0165079106461819,-0.0353321005215667,-0.00699377303329591));
#7264=CARTESIAN_POINT('',(0.0160769945899837,-0.0331915595474134,-0.00699377303329591));
#7265=CARTESIAN_POINT('',(0.0160769945899837,-0.0331915595474134,-0.00699377303329591));
#7266=CARTESIAN_POINT('',(0.0479406149651572,-0.0267770382679513,-0.00699377303329591));
#7267=CARTESIAN_POINT('',(0.015488900520983,-0.0285998427806792,-0.00699377303329591));
#7268=CARTESIAN_POINT('',(0.015488900520983,-0.0285998427806792,-0.01200000032));
#7269=CARTESIAN_POINT('',(0.015488900520983,-0.0285998427806792,0.00699377303329588));
#7270=CARTESIAN_POINT('',(0.0479406149651572,-0.0267770382679513,0.00699377303329588));
#7271=CARTESIAN_POINT('',(0.0160769945899843,-0.0331915595474165,0.00699377303329588));
#7272=CARTESIAN_POINT('',(0.0160769945899843,-0.0331915595474165,0.00699377303329588));
#7273=CARTESIAN_POINT('',(0.0165079106461826,-0.0353321005215691,0.00699377303329633));
#7274=CARTESIAN_POINT('',(0.0177795515520174,-0.0394021413608423,0.00790667524421404));
#7275=CARTESIAN_POINT('',(0.0196876809355332,-0.0429829534203928,0.00944920348110608));
#7276=CARTESIAN_POINT('',(0.0208497874735458,-0.0447359762231199,0.0100000004));
#7277=CARTESIAN_POINT('',(0.0138387927084345,0.000777321452246679,-0.01200000032));
#7278=CARTESIAN_POINT('',(0.0116025410900705,0.0405897085940067,-0.0069937730332959));
#7279=CARTESIAN_POINT('',(0.0138387927084345,0.000777321452246678,0.00699377303329589));
#7280=CARTESIAN_POINT('',(-0.0138387927084345,0.000777321452246679,-0.01200000032));
#7281=CARTESIAN_POINT('',(-0.0138387927084345,0.000777321452246679,-0.00699377303329591));
#7282=CARTESIAN_POINT('',(-0.0116025410900705,0.0405897085940067,0.00699377303329589));
#7283=CARTESIAN_POINT('',(0.,0.06842,-0.01200000032));
#7284=CARTESIAN_POINT('',(0.,0.06842,-0.0120000004));
#7285=CARTESIAN_POINT('',(-0.011,0.06842,-0.0120000004));
#7286=CARTESIAN_POINT('',(0.,0.06842,0.0120000004));
#7287=CARTESIAN_POINT('',(0.011,0.06842,0.0120000004));
#7288=CARTESIAN_POINT('',(-0.010444143618364,0.000586644879791539,0.0016));
#7289=CARTESIAN_POINT('',(-0.008207892,0.0403990320215515,0.0016));
#7290=CARTESIAN_POINT('',(-0.008207892,0.0403990320215515,0.0026));
#7291=CARTESIAN_POINT('',(-0.008207892,0.0403990320215515,0.00699377303329589));
#7292=CARTESIAN_POINT('',(-0.010444143618364,0.000586644879791538,0.00699377303329588));
#7293=CARTESIAN_POINT('',(-0.0114910488,-0.0180515951329767,0.00699377303329588));
#7294=CARTESIAN_POINT('',(-0.0114910488,-0.0180515951329767,0.0016));
#7295=CARTESIAN_POINT('',(-0.0114910488,-0.0180515951329767,0.0026));
#7296=CARTESIAN_POINT('',(-0.010444143618364,0.000586644879791539,0.0026));
#7297=CARTESIAN_POINT('',(0.,0.0403990320215515,0.0016));
#7298=CARTESIAN_POINT('',(-7.73280731427145E-5,0.0486065597524074,0.00790817554892985));
#7299=CARTESIAN_POINT('',(-0.00248654459668742,0.0485838610692401,0.00789166359185419));
#7300=CARTESIAN_POINT('',(-0.0047401145182197,0.0475210284454703,0.00699377303329588));
#7301=CARTESIAN_POINT('',(-0.00629018600225436,0.0456718918851082,0.00699377303329589));
#7302=CARTESIAN_POINT('',(-7.73280731427158E-5,0.0486065597524074,0.00790817554893012));
#7303=CARTESIAN_POINT('',(-0.00629018600225436,0.0456718918851082,0.00699377303329589));
#7304=CARTESIAN_POINT('',(0.,0.0403990320215515,0.00699377303329589));
#7305=CARTESIAN_POINT('',(0.,0.0403990320215515,0.0026));
#7306=CARTESIAN_POINT('',(0.008207892,0.0403990320215515,0.0026));
#7307=CARTESIAN_POINT('',(0.008207892,0.0403990320215515,0.0016));
#7308=CARTESIAN_POINT('',(0.008207892,0.0403990320215515,0.00699377303329589));
#7309=CARTESIAN_POINT('',(0.,0.0403990320215515,0.00699377303329589));
#7310=CARTESIAN_POINT('',(0.00629018600225437,0.0456718918851082,0.00699377303329589));
#7311=CARTESIAN_POINT('',(0.00629018600225437,0.0456718918851082,0.00699377303329589));
#7312=CARTESIAN_POINT('',(0.00474011451821985,0.0475210284454701,0.00699377303329588));
#7313=CARTESIAN_POINT('',(0.00248654459668787,0.0485838610692399,0.00789166359185404));
#7314=CARTESIAN_POINT('',(7.73280731434021E-5,0.0486065597524074,0.00790817554892985));
#7315=CARTESIAN_POINT('',(7.73280731434013E-5,0.0486065597524074,0.00790817554892985));
#7316=CARTESIAN_POINT('',(7.73280731434192E-5,0.0486065597524074,0.00790817554893013));
#7317=CARTESIAN_POINT('',(2.57775496670895E-5,0.048607045441007,0.00790817554893013));
#7318=CARTESIAN_POINT('',(-2.57775496664051E-5,0.048607045441007,0.00790817554893013));
#7319=CARTESIAN_POINT('',(-7.73280731427348E-5,0.0486065597524074,0.00790817554893013));
#7320=CARTESIAN_POINT('',(0.010444143618364,0.000586644879791539,0.0016));
#7321=CARTESIAN_POINT('',(0.0114910488,-0.0180515951329767,0.0016));
#7322=CARTESIAN_POINT('',(0.0114910488,-0.0180515951329767,0.0026));
#7323=CARTESIAN_POINT('',(0.0114910488,-0.0180515951329767,0.00699377303329588));
#7324=CARTESIAN_POINT('',(0.008207892,0.0403990320215515,0.00699377303329589));
#7325=CARTESIAN_POINT('',(0.0114910488,-0.0180515951329768,0.0026));
#7326=CARTESIAN_POINT('',(0.,-0.0180515951329767,0.0016));
#7327=CARTESIAN_POINT('',(0.,-0.0180515951329767,0.00699377303329588));
#7328=CARTESIAN_POINT('',(-0.00205973384739541,-0.029356536486291,0.00699377303329588));
#7329=CARTESIAN_POINT('',(-0.00205973384739541,-0.029356536486291,0.00699377303329588));
#7330=CARTESIAN_POINT('',(-0.000686577949131805,-0.029606722276116,0.00699377303329588));
#7331=CARTESIAN_POINT('',(0.00068657794913181,-0.029606722276116,0.00699377303329588));
#7332=CARTESIAN_POINT('',(0.00205973384739542,-0.029356536486291,0.00699377303329588));
#7333=CARTESIAN_POINT('',(0.00205973384739541,-0.029356536486291,0.00699377303329588));
#7334=CARTESIAN_POINT('',(0.,-0.0180515951329767,0.00699377303329588));
#7335=CARTESIAN_POINT('',(0.,-0.0180515951329767,0.0026));
#7336=CARTESIAN_POINT('',(0.,0.,0.0016));
#7337=CARTESIAN_POINT('',(0.00720946579703808,0.0403429506767117,0.0016));
#7338=CARTESIAN_POINT('',(0.0104910129546957,-0.018079019727579,0.0016));
#7339=CARTESIAN_POINT('',(0.00720784085825531,0.0403718797522103,0.0016));
#7340=CARTESIAN_POINT('',(0.,0.0403990320215515,0.0016));
#7341=CARTESIAN_POINT('',(-0.00720784085825531,0.0403718797522103,0.0016));
#7342=CARTESIAN_POINT('',(-0.00944571741540203,0.000530563534951791,0.0016));
#7343=CARTESIAN_POINT('',(-0.0104910129546957,-0.018079019727579,0.0016));
#7344=CARTESIAN_POINT('',(0.,-0.0180515951329767,0.0016));
#7345=CARTESIAN_POINT('',(-0.010444143618364,0.000586644879791539,-0.0016));
#7346=CARTESIAN_POINT('',(-0.0114910488,-0.0180515951329767,-0.0016));
#7347=CARTESIAN_POINT('',(-0.0114910488,-0.0180515951329767,-0.0026));
#7348=CARTESIAN_POINT('',(-0.0114910488,-0.0180515951329767,-0.00699377303329591));
#7349=CARTESIAN_POINT('',(-0.010444143618364,0.000586644879791539,-0.00699377303329591));
#7350=CARTESIAN_POINT('',(-0.008207892,0.0403990320215515,-0.0069937730332959));
#7351=CARTESIAN_POINT('',(-0.008207892,0.0403990320215515,-0.0016));
#7352=CARTESIAN_POINT('',(-0.008207892,0.0403990320215515,-0.0026));
#7353=CARTESIAN_POINT('',(-0.0114910488,-0.0180515951329768,-0.0026));
#7354=CARTESIAN_POINT('',(0.,-0.0180515951329767,-0.0016));
#7355=CARTESIAN_POINT('',(0.0114910488,-0.0180515951329767,-0.0016));
#7356=CARTESIAN_POINT('',(0.0114910488,-0.0180515951329767,-0.0026));
#7357=CARTESIAN_POINT('',(0.0114910488,-0.0180515951329767,-0.00699377303329591));
#7358=CARTESIAN_POINT('',(0.,-0.0180515951329767,-0.00699377303329591));
#7359=CARTESIAN_POINT('',(0.00205973384739524,-0.029356536486291,-0.00699377303329591));
#7360=CARTESIAN_POINT('',(0.00205973384739524,-0.029356536486291,-0.00699377303329591));
#7361=CARTESIAN_POINT('',(0.000686577949131747,-0.029606722276116,-0.00699377303329591));
#7362=CARTESIAN_POINT('',(-0.000686577949131747,-0.029606722276116,-0.00699377303329591));
#7363=CARTESIAN_POINT('',(-0.00205973384739524,-0.029356536486291,-0.00699377303329591));
#7364=CARTESIAN_POINT('',(-0.00205973384739524,-0.029356536486291,-0.00699377303329591));
#7365=CARTESIAN_POINT('',(0.,-0.0180515951329767,-0.00699377303329591));
#7366=CARTESIAN_POINT('',(0.,-0.0180515951329767,-0.0026));
#7367=CARTESIAN_POINT('',(0.010444143618364,0.000586644879791539,-0.0016));
#7368=CARTESIAN_POINT('',(0.008207892,0.0403990320215515,-0.0016));
#7369=CARTESIAN_POINT('',(0.008207892,0.0403990320215515,-0.0026));
#7370=CARTESIAN_POINT('',(0.008207892,0.0403990320215515,-0.0069937730332959));
#7371=CARTESIAN_POINT('',(0.0114910488,-0.0180515951329767,-0.00699377303329591));
#7372=CARTESIAN_POINT('',(0.010444143618364,0.000586644879791539,-0.0026));
#7373=CARTESIAN_POINT('',(0.,0.0403990320215515,-0.0016));
#7374=CARTESIAN_POINT('',(7.73280731449155E-5,0.0486065597524074,-0.00790817554892985));
#7375=CARTESIAN_POINT('',(0.00248654459668886,0.0485838610692395,-0.00789166359185372));
#7376=CARTESIAN_POINT('',(0.00474011451822018,0.0475210284454697,-0.00699377303329589));
#7377=CARTESIAN_POINT('',(0.00629018600225436,0.0456718918851082,-0.0069937730332959));
#7378=CARTESIAN_POINT('',(7.73280731449167E-5,0.0486065597524074,-0.00790817554893012));
#7379=CARTESIAN_POINT('',(0.00629018600225436,0.0456718918851082,-0.0069937730332959));
#7380=CARTESIAN_POINT('',(0.,0.0403990320215515,-0.0069937730332959));
#7381=CARTESIAN_POINT('',(0.,0.0403990320215515,-0.0026));
#7382=CARTESIAN_POINT('',(0.,0.0403990320215515,-0.0069937730332959));
#7383=CARTESIAN_POINT('',(-0.00629018600225436,0.0456718918851082,-0.0069937730332959));
#7384=CARTESIAN_POINT('',(-0.00629018600225436,0.0456718918851082,-0.0069937730332959));
#7385=CARTESIAN_POINT('',(-0.00474011451822014,0.0475210284454698,-0.00699377303329589));
#7386=CARTESIAN_POINT('',(-0.00248654459668875,0.0485838610692395,-0.00789166359185376));
#7387=CARTESIAN_POINT('',(-7.73280731447373E-5,0.0486065597524074,-0.00790817554892985));
#7388=CARTESIAN_POINT('',(-7.73280731447357E-5,0.0486065597524074,-0.00790817554892985));
#7389=CARTESIAN_POINT('',(-7.73280731447314E-5,0.0486065597524073,-0.00790817554893013));
#7390=CARTESIAN_POINT('',(-2.57775496672397E-5,0.048607045441007,-0.00790817554893013));
#7391=CARTESIAN_POINT('',(2.57775496674173E-5,0.048607045441007,-0.00790817554893013));
#7392=CARTESIAN_POINT('',(7.7328073144909E-5,0.0486065597524073,-0.00790817554893013));
#7393=CARTESIAN_POINT('',(0.,0.,-0.0016));
#7394=CARTESIAN_POINT('',(0.00944571741540203,0.000530563534951791,-0.0016));
#7395=CARTESIAN_POINT('',(0.00720784085825524,0.0403718797522103,-0.0016));
#7396=CARTESIAN_POINT('',(0.0104910129546957,-0.018079019727579,-0.0016));
#7397=CARTESIAN_POINT('',(0.,-0.0180515951329767,-0.0016));
#7398=CARTESIAN_POINT('',(-0.0104910129546957,-0.018079019727579,-0.0016));
#7399=CARTESIAN_POINT('',(-0.00720946579703808,0.0403429506767117,-0.0016));
#7400=CARTESIAN_POINT('',(-0.00720784085825531,0.0403718797522103,-0.0016));
#7401=CARTESIAN_POINT('',(0.,0.0403990320215515,-0.0016));
#7402=CARTESIAN_POINT('',(0.,0.06842,-0.0179937730332959));
#7403=CARTESIAN_POINT('',(7.87045304632302E-5,0.0529340922159572,-0.0116357978393905));
#7404=CARTESIAN_POINT('',(8.12506199999854E-5,0.0519321483087437,-0.0104194415588719));
#7405=CARTESIAN_POINT('',(8.43928020623833E-5,0.0506415015783407,-0.00944944180385271));
#7406=CARTESIAN_POINT('',(8.76647539293995E-5,0.0492073273028014,-0.00882504461561704));
#7407=CARTESIAN_POINT('',(7.87045304645403E-5,0.0529340922159572,-0.0116357978393905));
#7408=CARTESIAN_POINT('',(8.76647539280907E-5,0.0492073273028014,-0.00882504461561705));
#7409=CARTESIAN_POINT('',(0.,0.06842,-0.0116357978393905));
#7410=CARTESIAN_POINT('',(0.0132493773070601,0.060402922273412,-0.0116357978393905));
#7411=CARTESIAN_POINT('',(0.0132493773070601,0.060402922273412,-0.0116357978393905));
#7412=CARTESIAN_POINT('',(0.0129415944843386,0.0593692724324227,-0.0113058495927241));
#7413=CARTESIAN_POINT('',(0.0123626737236228,0.0573528398286717,-0.0104792531774306));
#7414=CARTESIAN_POINT('',(0.0113509423413671,0.0532843354740351,-0.00880854902741558));
#7415=CARTESIAN_POINT('',(0.0108078930523586,0.0500332694111275,-0.0079937730332959));
#7416=CARTESIAN_POINT('',(0.0105921890504172,0.0477738844607486,-0.0079937730332959));
#7417=CARTESIAN_POINT('',(0.0070565442830717,0.0463143052920532,-0.0079937730332959));
#7418=CARTESIAN_POINT('',(0.00617530299378753,0.0472946724703006,-0.00799377303329589));
#7419=CARTESIAN_POINT('',(0.00398690985736663,0.0487289177719894,-0.00843903646475693));
#7420=CARTESIAN_POINT('',(0.00140037055543791,0.0491971093619505,-0.00881798832068754));
#7421=CARTESIAN_POINT('',(8.76647097163739E-5,0.0492073466820214,-0.00882505305278234));
#7422=CARTESIAN_POINT('',(0.03650000008,0.0452155333197847,-0.0179937730332959));
#7423=CARTESIAN_POINT('',(-7.87045304632302E-5,0.0529340922159572,-0.0116357978393905));
#7424=CARTESIAN_POINT('',(-8.12506199999854E-5,0.0519321483087437,-0.0104194415588719));
#7425=CARTESIAN_POINT('',(-8.43928020623833E-5,0.0506415015783407,-0.00944944180385271));
#7426=CARTESIAN_POINT('',(-8.76647539293995E-5,0.0492073273028014,-0.00882504461561704));
#7427=CARTESIAN_POINT('',(-7.87045304645403E-5,0.0529340922159572,-0.0116357978393905));
#7428=CARTESIAN_POINT('',(-8.76647539283538E-5,0.0492073273028014,-0.00882504461561705));
#7429=CARTESIAN_POINT('',(0.03650000008,0.0529340922159572,-0.0116357978393905));
#7430=CARTESIAN_POINT('',(8.76647539280948E-5,0.0492073273028014,-0.00882504461561705));
#7431=CARTESIAN_POINT('',(2.92215846425317E-5,0.0492078331572327,-0.00882526484971964));
#7432=CARTESIAN_POINT('',(-2.92215846429342E-5,0.0492078331572327,-0.00882526484971964));
#7433=CARTESIAN_POINT('',(-8.76647539283029E-5,0.0492073273028014,-0.00882504461561705));
#7434=CARTESIAN_POINT('',(0.,0.06842,-0.0179937730332959));
#7435=CARTESIAN_POINT('',(-0.0105921890504172,0.0477738844607486,-0.0079937730332959));
#7436=CARTESIAN_POINT('',(-0.0108078930523586,0.0500332694111275,-0.0079937730332959));
#7437=CARTESIAN_POINT('',(-0.0113509423413671,0.0532843354740351,-0.0088085490274156));
#7438=CARTESIAN_POINT('',(-0.0123626737236227,0.0573528398286717,-0.0104792531774306));
#7439=CARTESIAN_POINT('',(-0.0129415944843386,0.0593692724324227,-0.0113058495927241));
#7440=CARTESIAN_POINT('',(-0.0132493773070601,0.0604029222734119,-0.0116357978393905));
#7441=CARTESIAN_POINT('',(-0.0132493773070601,0.0604029222734119,-0.0116357978393905));
#7442=CARTESIAN_POINT('',(0.,0.06842,-0.0116357978393905));
#7443=CARTESIAN_POINT('',(-8.76647097176486E-5,0.0492073466820214,-0.00882505305278234));
#7444=CARTESIAN_POINT('',(-0.00140037055543896,0.0491971093619503,-0.00881798832068744));
#7445=CARTESIAN_POINT('',(-0.00398690985736713,0.0487289177719891,-0.0084390364647568));
#7446=CARTESIAN_POINT('',(-0.00617530299378768,0.0472946724703004,-0.00799377303329589));
#7447=CARTESIAN_POINT('',(-0.0070565442830717,0.0463143052920532,-0.0079937730332959));
#7448=CARTESIAN_POINT('',(0.,0.06842,0.0179937730332959));
#7449=CARTESIAN_POINT('',(-7.87045304628983E-5,0.0529340922159572,0.0116357978393905));
#7450=CARTESIAN_POINT('',(-8.12506199994636E-5,0.0519321483087437,0.0104194415588719));
#7451=CARTESIAN_POINT('',(-8.43928020608055E-5,0.0506415015783407,0.00944944180385272));
#7452=CARTESIAN_POINT('',(-8.76647539264997E-5,0.0492073273028014,0.00882504461561704));
#7453=CARTESIAN_POINT('',(-7.87045304633841E-5,0.0529340922159572,0.0116357978393905));
#7454=CARTESIAN_POINT('',(-8.76647539263809E-5,0.0492073273028014,0.00882504461561705));
#7455=CARTESIAN_POINT('',(0.,0.06842,0.0116357978393905));
#7456=CARTESIAN_POINT('',(-0.0132493773070601,0.060402922273412,0.0116357978393905));
#7457=CARTESIAN_POINT('',(-0.0132493773070601,0.060402922273412,0.0116357978393905));
#7458=CARTESIAN_POINT('',(-0.0129415944843387,0.0593692724324228,0.0113058495927241));
#7459=CARTESIAN_POINT('',(-0.0123626737236229,0.057352839828672,0.0104792531774307));
#7460=CARTESIAN_POINT('',(-0.0113509423413671,0.0532843354740351,0.00880854902741569));
#7461=CARTESIAN_POINT('',(-0.0108078930523591,0.0500332694111306,0.00799377303329642));
#7462=CARTESIAN_POINT('',(-0.0105921890504176,0.0477738844607519,0.00799377303329589));
#7463=CARTESIAN_POINT('',(-0.0070565442830717,0.0463143052920532,0.00799377303329589));
#7464=CARTESIAN_POINT('',(-0.00617530299378738,0.0472946724703008,0.00799377303329588));
#7465=CARTESIAN_POINT('',(-0.00398690985736601,0.0487289177719897,0.0084390364647571));
#7466=CARTESIAN_POINT('',(-0.00140037055543677,0.0491971093619506,0.00881798832068766));
#7467=CARTESIAN_POINT('',(-8.76647097150039E-5,0.0492073466820214,0.00882505305278234));
#7468=CARTESIAN_POINT('',(0.03650000008,0.0452155333197847,0.0179937730332959));
#7469=CARTESIAN_POINT('',(7.87045304628983E-5,0.0529340922159572,0.0116357978393905));
#7470=CARTESIAN_POINT('',(8.12506199994635E-5,0.0519321483087437,0.0104194415588719));
#7471=CARTESIAN_POINT('',(8.43928020602378E-5,0.0506415015783407,0.00944944180385273));
#7472=CARTESIAN_POINT('',(8.76647539255388E-5,0.0492073273028014,0.00882504461561705));
#7473=CARTESIAN_POINT('',(7.8704530463384E-5,0.0529340922159572,0.0116357978393905));
#7474=CARTESIAN_POINT('',(8.76647539276827E-5,0.0492073273028014,0.00882504461561705));
#7475=CARTESIAN_POINT('',(0.03650000008,0.0529340922159572,0.0116357978393905));
#7476=CARTESIAN_POINT('',(-8.76647539264086E-5,0.0492073273028014,0.00882504461561705));
#7477=CARTESIAN_POINT('',(-2.92215846419373E-5,0.0492078331572327,0.00882526484971964));
#7478=CARTESIAN_POINT('',(2.92215846421801E-5,0.0492078331572327,0.00882526484971964));
#7479=CARTESIAN_POINT('',(8.76647539259437E-5,0.0492073273028014,0.00882504461561705));
#7480=CARTESIAN_POINT('',(0.,0.06842,0.0179937730332959));
#7481=CARTESIAN_POINT('',(0.0105921890504172,0.0477738844607486,0.00799377303329589));
#7482=CARTESIAN_POINT('',(0.0108078930523586,0.0500332694111275,0.00799377303329589));
#7483=CARTESIAN_POINT('',(0.0113509423413671,0.0532843354740351,0.0088085490274156));
#7484=CARTESIAN_POINT('',(0.0123626737236227,0.0573528398286717,0.0104792531774306));
#7485=CARTESIAN_POINT('',(0.0129415944843386,0.0593692724324227,0.0113058495927241));
#7486=CARTESIAN_POINT('',(0.0132493773070601,0.060402922273412,0.0116357978393905));
#7487=CARTESIAN_POINT('',(0.0132493773070601,0.060402922273412,0.0116357978393905));
#7488=CARTESIAN_POINT('',(0.,0.06842,0.0116357978393905));
#7489=CARTESIAN_POINT('',(8.76647097150728E-5,0.0492073466820214,0.00882505305278234));
#7490=CARTESIAN_POINT('',(0.00140037055543682,0.0491971093619506,0.00881798832068765));
#7491=CARTESIAN_POINT('',(0.00398690985736599,0.0487289177719897,0.0084390364647571));
#7492=CARTESIAN_POINT('',(0.00617530299378739,0.0472946724703008,0.00799377303329588));
#7493=CARTESIAN_POINT('',(0.0070565442830717,0.0463143052920532,0.00799377303329589));
#7494=CARTESIAN_POINT('',(0.,-0.0684221052,-0.0179937730332959));
#7495=CARTESIAN_POINT('',(0.0150966619928098,-0.0333889120212215,-0.00799377303329591));
#7496=CARTESIAN_POINT('',(0.0156245563131541,-0.0355097001088308,-0.00799377303329591));
#7497=CARTESIAN_POINT('',(0.0171293719837654,-0.0395124805465279,-0.00887297982396414));
#7498=CARTESIAN_POINT('',(0.0192473600818881,-0.0430417062190822,-0.0102455541943977));
#7499=CARTESIAN_POINT('',(0.020465779284996,-0.044769026527585,-0.0107267070030277));
#7500=CARTESIAN_POINT('',(0.020465779284996,-0.044769026527585,-0.0107267070030277));
#7501=CARTESIAN_POINT('',(0.,-0.0684221052,-0.0107267070030269));
#7502=CARTESIAN_POINT('',(-0.0204657792849939,-0.044769026527582,-0.0107267070030269));
#7503=CARTESIAN_POINT('',(-0.0204657792849939,-0.044769026527582,-0.0107267070030269));
#7504=CARTESIAN_POINT('',(-0.0192473600818865,-0.0430417062190796,-0.0102455541943968));
#7505=CARTESIAN_POINT('',(-0.0171293719837647,-0.0395124805465262,-0.00887297982396364));
#7506=CARTESIAN_POINT('',(-0.0156245563131539,-0.0355097001088302,-0.00799377303329591));
#7507=CARTESIAN_POINT('',(-0.0150966619928098,-0.0333889120212215,-0.00799377303329591));
#7508=CARTESIAN_POINT('',(-0.00223898065795575,-0.0303403406237615,-0.00799377303329591));
#7509=CARTESIAN_POINT('',(-0.000746326885985252,-0.0305800173967141,-0.00799377303329591));
#7510=CARTESIAN_POINT('',(0.000746326885985252,-0.0305800173967141,-0.0079937730332959));
#7511=CARTESIAN_POINT('',(0.00223898065795575,-0.0303403406237615,-0.0079937730332959));
#7512=CARTESIAN_POINT('',(0.,-0.0684221052,0.0179937730332959));
#7513=CARTESIAN_POINT('',(-0.0150966619928097,-0.0333889120212214,0.00799377303329588));
#7514=CARTESIAN_POINT('',(-0.015624556313154,-0.0355097001088307,0.00799377303329588));
#7515=CARTESIAN_POINT('',(-0.0171293719837654,-0.0395124805465279,0.00887297982396415));
#7516=CARTESIAN_POINT('',(-0.019247360081888,-0.0430417062190821,0.0102455541943978));
#7517=CARTESIAN_POINT('',(-0.020465779284996,-0.0447690265275849,0.0107267070030278));
#7518=CARTESIAN_POINT('',(-0.020465779284996,-0.0447690265275849,0.0107267070030277));
#7519=CARTESIAN_POINT('',(0.,-0.0684221052,0.0107267070030269));
#7520=CARTESIAN_POINT('',(0.0204657792849938,-0.0447690265275819,0.0107267070030269));
#7521=CARTESIAN_POINT('',(0.0204657792849938,-0.0447690265275819,0.0107267070030269));
#7522=CARTESIAN_POINT('',(0.0192473600818866,-0.0430417062190798,0.0102455541943969));
#7523=CARTESIAN_POINT('',(0.0171293719837646,-0.0395124805465257,0.00887297982396374));
#7524=CARTESIAN_POINT('',(0.0156245563131549,-0.0355097001088332,0.00799377303329635));
#7525=CARTESIAN_POINT('',(0.0150966619928105,-0.0333889120212248,0.00799377303329588));
#7526=CARTESIAN_POINT('',(0.00223898065795594,-0.0303403406237614,0.00799377303329588));
#7527=CARTESIAN_POINT('',(0.000746326885985315,-0.0305800173967141,0.00799377303329588));
#7528=CARTESIAN_POINT('',(-0.000746326885985315,-0.0305800173967141,0.00799377303329587));
#7529=CARTESIAN_POINT('',(-0.00223898065795594,-0.0303403406237614,0.00799377303329587));
#7530=CARTESIAN_POINT('',(0.,-0.0180515951329767,0.0026));
#7531=CARTESIAN_POINT('',(-0.0114910488,-0.0180515951329767,0.0026));
#7532=CARTESIAN_POINT('',(-0.0114910488,-0.0180515951329767,0.00233582142178957));
#7533=CARTESIAN_POINT('',(-0.0112753897480323,-0.018057692716622,0.00181816981976291));
#7534=CARTESIAN_POINT('',(-0.010751370193641,-0.0180720491888493,0.00159999999999997));
#7535=CARTESIAN_POINT('',(-0.0104910129546955,-0.018079019727579,0.0016));
#7536=CARTESIAN_POINT('',(0.0114910488,-0.0180515951329767,0.0026));
#7537=CARTESIAN_POINT('',(0.0114910488,-0.0180515951329767,0.00233582142178958));
#7538=CARTESIAN_POINT('',(0.0112753897480323,-0.0180576927166228,0.00181816981976292));
#7539=CARTESIAN_POINT('',(0.010751370193641,-0.0180720491888478,0.00159999999999997));
#7540=CARTESIAN_POINT('',(0.0104910129546956,-0.018079019727579,0.0016));
#7541=CARTESIAN_POINT('',(0.00944571741540203,0.000530563534951791,0.0026));
#7542=CARTESIAN_POINT('',(0.008207892,0.0403990320215515,0.0026));
#7543=CARTESIAN_POINT('',(0.008207892,0.0403990320215515,0.00233582041202305));
#7544=CARTESIAN_POINT('',(0.00799223219364738,0.0403929152387224,0.00181816659020097));
#7545=CARTESIAN_POINT('',(0.0074682025896938,0.0403787024449846,0.00160000000000004));
#7546=CARTESIAN_POINT('',(0.0072078408582554,0.0403718797522114,0.0016));
#7547=CARTESIAN_POINT('',(-0.00944571741540203,0.000530563534951791,0.0026));
#7548=CARTESIAN_POINT('',(-0.008207892,0.0403990320215515,0.0026));
#7549=CARTESIAN_POINT('',(-0.008207892,0.0403990320215515,0.00233582041202305));
#7550=CARTESIAN_POINT('',(-0.00799223219364738,0.0403929152387224,0.00181816659020097));
#7551=CARTESIAN_POINT('',(-0.0074682025896938,0.0403787024449846,0.00160000000000004));
#7552=CARTESIAN_POINT('',(-0.0072078408582554,0.0403718797522114,0.0016));
#7553=CARTESIAN_POINT('',(0.,0.0403990320215515,0.0026));
#7554=CARTESIAN_POINT('',(0.,0.,0.0130000004));
#7555=CARTESIAN_POINT('',(0.,0.06842,0.0130000004));
#7556=CARTESIAN_POINT('',(0.012,0.06842,0.0130000004));
#7557=CARTESIAN_POINT('',(0.,0.06842,0.0130000004));
#7558=CARTESIAN_POINT('',(0.0122,0.06842,0.0130000004));
#7559=CARTESIAN_POINT('',(0.,0.,-0.0130000004));
#7560=CARTESIAN_POINT('',(0.,0.06842,-0.0130000004));
#7561=CARTESIAN_POINT('',(-0.012,0.06842,-0.0130000004));
#7562=CARTESIAN_POINT('',(0.,0.06842,-0.0130000004));
#7563=CARTESIAN_POINT('',(0.0122,0.06842,-0.0130000004));
#7564=CARTESIAN_POINT('',(0.,-0.0180515951329767,-0.00699377303329591));
#7565=CARTESIAN_POINT('',(-0.00223898065795575,-0.0303403406237615,-0.00699377303329591));
#7566=CARTESIAN_POINT('',(-0.0114910488,-0.0180515951329767,-0.00699377303329591));
#7567=CARTESIAN_POINT('',(-0.0114910488,-0.0180515951329767,-0.0072579473393628));
#7568=CARTESIAN_POINT('',(-0.011706704997243,-0.0180455852288076,-0.00777558982005122));
#7569=CARTESIAN_POINT('',(-0.0122306785725227,-0.018030548260386,-0.00799377303329577));
#7570=CARTESIAN_POINT('',(-0.0124910159490166,-0.0180229475260996,-0.00799377303329591));
#7571=CARTESIAN_POINT('',(-0.00834780990288846,0.055739290033391,-0.0069937730332959));
#7572=CARTESIAN_POINT('',(-0.008207892,0.0403990320215515,-0.0069937730332959));
#7573=CARTESIAN_POINT('',(-0.008207892,0.0403990320215515,-0.00725794661302549));
#7574=CARTESIAN_POINT('',(-0.0084235477697883,0.0404050261404904,-0.00777558759299344));
#7575=CARTESIAN_POINT('',(-0.00894751289069499,0.0404201914761733,-0.00799377303329587));
#7576=CARTESIAN_POINT('',(-0.00920784674600953,0.0404279004413884,-0.0079937730332959));
#7577=CARTESIAN_POINT('',(0.00223898065795575,-0.0303403406237615,-0.00799377303329591));
#7578=CARTESIAN_POINT('',(0.00205973384739524,-0.029356536486291,-0.00799377303329591));
#7579=CARTESIAN_POINT('',(0.00205973384739524,-0.029356536486291,-0.00699377303329591));
#7580=CARTESIAN_POINT('',(0.000748242919122894,-0.0305797097356639,-0.00799377303329591));
#7581=CARTESIAN_POINT('',(0.000715497284703133,-0.0296014532411425,-0.00796255052786754));
#7582=CARTESIAN_POINT('',(0.000686577949441513,-0.0296067222760596,-0.00699377303671879));
#7583=CARTESIAN_POINT('',(-0.000748242919126098,-0.0305797097356639,-0.00799377303329591));
#7584=CARTESIAN_POINT('',(-0.000715497284704723,-0.0296014532411425,-0.00796255052786754));
#7585=CARTESIAN_POINT('',(-0.00068657794944333,-0.0296067222760592,-0.00699377303671879));
#7586=CARTESIAN_POINT('',(-0.00223898065795575,-0.0303403406237615,-0.00799377303329591));
#7587=CARTESIAN_POINT('',(-0.00205973384739524,-0.029356536486291,-0.00799377303329591));
#7588=CARTESIAN_POINT('',(-0.00205973384739524,-0.029356536486291,-0.00699377303329591));
#7589=CARTESIAN_POINT('',(0.00223898065795575,-0.0303403406237615,-0.00699377303329591));
#7590=CARTESIAN_POINT('',(0.,0.0403990320215515,-0.0069937730332959));
#7591=CARTESIAN_POINT('',(-0.0070565442830717,0.0463143052920532,-0.0069937730332959));
#7592=CARTESIAN_POINT('',(0.,-0.0180515951329767,-0.00699377303329591));
#7593=CARTESIAN_POINT('',(0.0114910488,-0.0180515951329767,-0.00699377303329591));
#7594=CARTESIAN_POINT('',(0.0114910488,-0.0180515951329767,-0.00725794733936287));
#7595=CARTESIAN_POINT('',(0.0117067049972432,-0.018045585228809,-0.00777558982005143));
#7596=CARTESIAN_POINT('',(0.0122306785725229,-0.018030548260383,-0.00799377303329588));
#7597=CARTESIAN_POINT('',(0.0124910159490171,-0.0180229475260996,-0.00799377303329591));
#7598=CARTESIAN_POINT('',(-0.0070565442830717,0.0463143052920532,-0.0079937730332959));
#7599=CARTESIAN_POINT('',(-0.00629018600225436,0.0456718918851082,-0.00799377303329591));
#7600=CARTESIAN_POINT('',(-0.00629018600225436,0.0456718918851082,-0.0069937730332959));
#7601=CARTESIAN_POINT('',(-0.00663675715233594,0.0467813119196923,-0.0079937730332959));
#7602=CARTESIAN_POINT('',(-0.00593832363413277,0.0460916412822681,-0.0079723098444523));
#7603=CARTESIAN_POINT('',(-0.00590046854092345,0.0461367999963669,-0.006993773037332));
#7604=CARTESIAN_POINT('',(-0.0056995674399402,0.0476010156616628,-0.00809040380897162));
#7605=CARTESIAN_POINT('',(-0.00516716899465654,0.0468516022761799,-0.00800170584891996));
#7606=CARTESIAN_POINT('',(-0.00503969845558171,0.0469583719208727,-0.00710006688468518));
#7607=CARTESIAN_POINT('',(-0.00343035019733571,0.048822457084395,-0.00851824659842761));
#7608=CARTESIAN_POINT('',(-0.00322701332654168,0.0481104007221522,-0.00828757882417036));
#7609=CARTESIAN_POINT('',(-0.00299842737141113,0.0482019239037002,-0.00757069395613868));
#7610=CARTESIAN_POINT('',(-0.00140299443024509,0.0492029057968726,-0.00882198790030471));
#7611=CARTESIAN_POINT('',(-0.00128861423874107,0.048601413833971,-0.00856090079419736));
#7612=CARTESIAN_POINT('',(-0.00122463996233032,0.0486019331129095,-0.00790480938657816));
#7613=CARTESIAN_POINT('',(-3.88600902706837E-5,0.0492076213378734,-0.00882524260713517));
#7614=CARTESIAN_POINT('',(-3.56761871707623E-5,0.048606846674528,-0.00856365092865193));
#7615=CARTESIAN_POINT('',(-3.3919989452083E-5,0.0486068539322644,-0.00790838956451909));
#7616=CARTESIAN_POINT('',(-7.73280731625782E-5,0.0486067841404136,-0.00790817557838339));
#7617=CARTESIAN_POINT('',(-7.79525636419675E-5,0.0486067680811581,-0.00803052154214757));
#7618=CARTESIAN_POINT('',(-8.02997886509625E-5,0.0486476233580726,-0.00835342390755972));
#7619=CARTESIAN_POINT('',(-8.48435892314036E-5,0.0489650114210101,-0.00871946462590189));
#7620=CARTESIAN_POINT('',(-8.76646190459199E-5,0.0492073271001888,-0.00882504508381696));
#7621=CARTESIAN_POINT('',(0.0114425698213259,0.000642726224631287,-0.00699377303329591));
#7622=CARTESIAN_POINT('',(0.008207892,0.0403990320215515,-0.0069937730332959));
#7623=CARTESIAN_POINT('',(0.008207892,0.0403990320215515,-0.00725794661302555));
#7624=CARTESIAN_POINT('',(0.00842354776978842,0.04040502614049,-0.00777558759299362));
#7625=CARTESIAN_POINT('',(0.00894751289069526,0.0404201914761742,-0.00799377303329597));
#7626=CARTESIAN_POINT('',(0.00920784674600989,0.0404279004413884,-0.0079937730332959));
#7627=CARTESIAN_POINT('',(2.64772969592201E-7,0.0496067633136083,-0.00790830685388911));
#7628=CARTESIAN_POINT('',(8.76646190442611E-5,0.0492073271002133,-0.00882504508376052));
#7629=CARTESIAN_POINT('',(8.48436080713886E-5,0.0489650130516421,-0.00871946530317839));
#7630=CARTESIAN_POINT('',(8.02998525257403E-5,0.0486476250247848,-0.008353427333427));
#7631=CARTESIAN_POINT('',(7.79525723050023E-5,0.0486067681697317,-0.00803052328677894));
#7632=CARTESIAN_POINT('',(7.73280728928411E-5,0.0486067842334127,-0.00790817557840466));
#7633=CARTESIAN_POINT('',(0.,0.0403990320215515,-0.0069937730332959));
#7634=CARTESIAN_POINT('',(0.0070565442830717,0.0463143052920532,-0.0069937730332959));
#7635=CARTESIAN_POINT('',(0.00629018600225436,0.0456718918851082,-0.0069937730332959));
#7636=CARTESIAN_POINT('',(0.00629018600225436,0.0456718918851082,-0.00799377303329591));
#7637=CARTESIAN_POINT('',(0.0070565442830717,0.0463143052920532,-0.0079937730332959));
#7638=CARTESIAN_POINT('',(0.00590046854092339,0.0461367999963669,-0.006993773037332));
#7639=CARTESIAN_POINT('',(0.00593832363413271,0.0460916412822682,-0.0079723098444523));
#7640=CARTESIAN_POINT('',(0.00663675715233588,0.0467813119196924,-0.0079937730332959));
#7641=CARTESIAN_POINT('',(0.0050396984555815,0.0469583719208729,-0.00710006688468504));
#7642=CARTESIAN_POINT('',(0.00516716899465523,0.04685160227618,-0.00800170584891948));
#7643=CARTESIAN_POINT('',(0.00569956743993997,0.0476010156616624,-0.00809040380897139));
#7644=CARTESIAN_POINT('',(0.00299842737141054,0.0482019239037004,-0.00757069395613965));
#7645=CARTESIAN_POINT('',(0.00322701332654435,0.0481104007221538,-0.00828757882417294));
#7646=CARTESIAN_POINT('',(0.00343035019733507,0.0488224570843983,-0.00851824659842906));
#7647=CARTESIAN_POINT('',(0.00122463996232939,0.0486019331129096,-0.00790480938657469));
#7648=CARTESIAN_POINT('',(0.00128861423873465,0.0486014138339637,-0.00856090079418587));
#7649=CARTESIAN_POINT('',(0.00140299443024396,0.0492029057968596,-0.0088219879002991));
#7650=CARTESIAN_POINT('',(3.39199894509637E-5,0.0486068539322645,-0.0079083895645191));
#7651=CARTESIAN_POINT('',(3.56761871695851E-5,0.048606846674528,-0.00856365092865193));
#7652=CARTESIAN_POINT('',(3.88600902694015E-5,0.0492076213378734,-0.00882524260713517));
#7653=CARTESIAN_POINT('',(-0.0479406149651572,-0.0267770382679513,-0.0100000004));
#7654=CARTESIAN_POINT('',(-0.0200162970866488,-0.0452885101813074,-0.0100000004));
#7655=CARTESIAN_POINT('',(-0.03550000008,-0.0578844846861028,-0.0100000004));
#7656=CARTESIAN_POINT('',(-0.0150966619928097,-0.0333889120212215,-0.00799377303329591));
#7657=CARTESIAN_POINT('',(-0.0160769945899837,-0.0331915595474134,-0.00799377303329591));
#7658=CARTESIAN_POINT('',(-0.0160769945899837,-0.0331915595474134,-0.00699377303329591));
#7659=CARTESIAN_POINT('',(-0.0156068158481616,-0.0354384287075173,-0.00799377303329591));
#7660=CARTESIAN_POINT('',(-0.0164617445110731,-0.035102773952805,-0.00790249484159822));
#7661=CARTESIAN_POINT('',(-0.0165074089866533,-0.0353296085680631,-0.00699377303908019));
#7662=CARTESIAN_POINT('',(-0.0170663475656837,-0.039383215844906,-0.00882366076849526));
#7663=CARTESIAN_POINT('',(-0.0175691716233766,-0.0389007355739446,-0.00846666609674932));
#7664=CARTESIAN_POINT('',(-0.0177790331975686,-0.0394032662983781,-0.0079066495412633));
#7665=CARTESIAN_POINT('',(-0.0192020228604743,-0.0429774328463443,-0.0102276505555632));
#7666=CARTESIAN_POINT('',(-0.0195815577937006,-0.0428095980046082,-0.00992665585498258));
#7667=CARTESIAN_POINT('',(-0.0196915521790689,-0.0429887931415983,-0.00945103830350947));
#7668=CARTESIAN_POINT('',(-0.0204657792849939,-0.044769026527582,-0.0107267070030269));
#7669=CARTESIAN_POINT('',(-0.0207883947143825,-0.0446433660335933,-0.0104373351105851));
#7670=CARTESIAN_POINT('',(-0.0208497874735458,-0.04473597622312,-0.0100000004));
#7671=CARTESIAN_POINT('',(-0.0200162970866488,-0.0452885101813074,-0.0100000004));
#7672=CARTESIAN_POINT('',(-0.0150966619928098,-0.0333889120212215,-0.00699377303329591));
#7673=CARTESIAN_POINT('',(-0.0479406149651572,-0.0267770382679513,-0.00699377303329591));
#7674=CARTESIAN_POINT('',(-0.0144904743180211,-0.028655924125519,-0.00699377303329591));
#7675=CARTESIAN_POINT('',(-0.00974560658703515,0.0558178039161666,-0.0069937730332959));
#7676=CARTESIAN_POINT('',(-0.0106041148871086,0.0405336272491669,-0.0069937730332959));
#7677=CARTESIAN_POINT('',(-0.0770011542117716,0.0442631319913884,-0.0069937730332959));
#7678=CARTESIAN_POINT('',(-0.0105921890504172,0.0477738844607486,-0.0069937730332959));
#7679=CARTESIAN_POINT('',(-0.0115907945846862,0.0477210925397055,-0.0069937730332959));
#7680=CARTESIAN_POINT('',(-0.0115907945846862,0.0477210925397055,-0.0079937730332959));
#7681=CARTESIAN_POINT('',(-0.0105921890504172,0.0477738844607486,-0.0079937730332959));
#7682=CARTESIAN_POINT('',(-0.01165154122072,0.0488701684917268,-0.00699377303594161));
#7683=CARTESIAN_POINT('',(-0.0116460760642758,0.0487667902637238,-0.00794865545244461));
#7684=CARTESIAN_POINT('',(-0.0106957683040226,0.0488588221723721,-0.0079937730332959));
#7685=CARTESIAN_POINT('',(-0.0118303126054588,0.0511152954428173,-0.00726680033960579));
#7686=CARTESIAN_POINT('',(-0.0118031703322195,0.0508361592339155,-0.00808736980036333));
#7687=CARTESIAN_POINT('',(-0.0109685466035931,0.0509905050542695,-0.0082419796763848));
#7688=CARTESIAN_POINT('',(-0.0122589931203777,0.054381431806862,-0.00828727294311499));
#7689=CARTESIAN_POINT('',(-0.0122076213027984,0.0540496545607623,-0.0089013378879519));
#7690=CARTESIAN_POINT('',(-0.0115702429201374,0.0541479034369538,-0.00916968204236862));
#7691=CARTESIAN_POINT('',(-0.0128211649345838,0.0574770135698705,-0.00966421320592845));
#7692=CARTESIAN_POINT('',(-0.0127613931441634,0.0571911655524021,-0.010111758697774));
#7693=CARTESIAN_POINT('',(-0.0123263746292068,0.0572218599509659,-0.0104214459159332));
#7694=CARTESIAN_POINT('',(-0.0132893215582587,0.0595090645092476,-0.0106162645372993));
#7695=CARTESIAN_POINT('',(-0.0132467806557753,0.0593347911246909,-0.0110069763062972));
#7696=CARTESIAN_POINT('',(-0.0129239618696845,0.0593100555036758,-0.0112869471314198));
#7697=CARTESIAN_POINT('',(-0.0135575831556229,0.0605538020003774,-0.0110000003200065));
#7698=CARTESIAN_POINT('',(-0.0135257202877438,0.0604297129284592,-0.0113656106861467));
#7699=CARTESIAN_POINT('',(-0.0132493773070656,0.0604029222734306,-0.0116357978393965));
#7700=CARTESIAN_POINT('',(-0.0125890041486941,0.0608025080665215,-0.0110000003200065));
#7701=CARTESIAN_POINT('',(0.0479406149651572,-0.0267770382679513,-0.0100000004));
#7702=CARTESIAN_POINT('',(0.03550000008,-0.0578844846861028,-0.0100000004));
#7703=CARTESIAN_POINT('',(0.0200162970866488,-0.0452885101813074,-0.0100000004));
#7704=CARTESIAN_POINT('',(0.0160769945899837,-0.0331915595474134,-0.00699377303329591));
#7705=CARTESIAN_POINT('',(0.0160769945899837,-0.0331915595474134,-0.00799377303329591));
#7706=CARTESIAN_POINT('',(0.0150966619928097,-0.0333889120212215,-0.00799377303329591));
#7707=CARTESIAN_POINT('',(0.0165074089866533,-0.0353296085680631,-0.00699377303908019));
#7708=CARTESIAN_POINT('',(0.0164617445110731,-0.035102773952805,-0.00790249484159823));
#7709=CARTESIAN_POINT('',(0.0156068158481616,-0.0354384287075173,-0.00799377303329591));
#7710=CARTESIAN_POINT('',(0.0177790331975681,-0.0394032662983772,-0.00790664954127394));
#7711=CARTESIAN_POINT('',(0.0175691716233725,-0.0389007355739614,-0.00846666609676319));
#7712=CARTESIAN_POINT('',(0.0170663475656786,-0.0393832158449129,-0.00882366076850327));
#7713=CARTESIAN_POINT('',(0.01969155217907,-0.0429887931416,-0.00945103830348819));
#7714=CARTESIAN_POINT('',(0.019581557793716,-0.0428095980045924,-0.00992665585496257));
#7715=CARTESIAN_POINT('',(0.0192020228604844,-0.0429774328463306,-0.0102276505555471));
#7716=CARTESIAN_POINT('',(0.0208497874735458,-0.04473597622312,-0.0100000004));
#7717=CARTESIAN_POINT('',(0.0207883947143824,-0.0446433660335932,-0.0104373351105851));
#7718=CARTESIAN_POINT('',(0.0204657792849938,-0.0447690265275819,-0.0107267070030269));
#7719=CARTESIAN_POINT('',(0.0200162970866488,-0.0452885101813074,-0.0100000004));
#7720=CARTESIAN_POINT('',(0.0150966619928098,-0.0333889120212215,-0.00699377303329591));
#7721=CARTESIAN_POINT('',(0.0479406149651572,-0.0267770382679513,-0.00699377303329591));
#7722=CARTESIAN_POINT('',(0.0144904743180211,-0.028655924125519,-0.00699377303329591));
#7723=CARTESIAN_POINT('',(0.0128403665054726,0.000721240107406931,-0.00699377303329591));
#7724=CARTESIAN_POINT('',(0.0106041148871086,0.0405336272491669,-0.0069937730332959));
#7725=CARTESIAN_POINT('',(0.0770011542117716,0.0442631319913884,-0.0069937730332959));
#7726=CARTESIAN_POINT('',(0.0105921890504172,0.0477738844607486,-0.0069937730332959));
#7727=CARTESIAN_POINT('',(0.0105921890504172,0.0477738844607486,-0.0079937730332959));
#7728=CARTESIAN_POINT('',(0.0115907945846862,0.0477210925397055,-0.0079937730332959));
#7729=CARTESIAN_POINT('',(0.0115907945846862,0.0477210925397055,-0.0069937730332959));
#7730=CARTESIAN_POINT('',(0.0106957683040225,0.0488588221723706,-0.0079937730332959));
#7731=CARTESIAN_POINT('',(0.0116460760642757,0.0487667902637224,-0.00794865545244467));
#7732=CARTESIAN_POINT('',(0.01165154122072,0.0488701684917252,-0.00699377303594161));
#7733=CARTESIAN_POINT('',(0.0109685466035914,0.0509905050542603,-0.00824197967638226));
#7734=CARTESIAN_POINT('',(0.0118031703322181,0.0508361592339046,-0.00808736980036114));
#7735=CARTESIAN_POINT('',(0.0118303126054573,0.0511152954428084,-0.0072668003396034));
#7736=CARTESIAN_POINT('',(0.0115702429201392,0.0541479034369613,-0.00916968204237201));
#7737=CARTESIAN_POINT('',(0.0122076213028006,0.0540496545607744,-0.00890133788795471));
#7738=CARTESIAN_POINT('',(0.01225899312038,0.0543814318068674,-0.00828727294311731));
#7739=CARTESIAN_POINT('',(0.0123263746291898,0.0572218599508923,-0.0104214459159037));
#7740=CARTESIAN_POINT('',(0.0127613931441495,0.0571911655523188,-0.0101117586977502));
#7741=CARTESIAN_POINT('',(0.0128211649345674,0.0574770135698036,-0.00966421320590118));
#7742=CARTESIAN_POINT('',(0.0129239618697091,0.0593100555037898,-0.0112869471314648));
#7743=CARTESIAN_POINT('',(0.0132467806557945,0.0593347911248174,-0.0110069763063276));
#7744=CARTESIAN_POINT('',(0.0132893215582847,0.0595090645093479,-0.0106162645373376));
#7745=CARTESIAN_POINT('',(0.0132493773070601,0.060402922273412,-0.0116357978393905));
#7746=CARTESIAN_POINT('',(0.0135257202877391,0.0604297129284408,-0.0113656106861407));
#7747=CARTESIAN_POINT('',(0.0135575831556184,0.0605538020003596,-0.01100000032));
#7748=CARTESIAN_POINT('',(0.0125890041486895,0.0608025080665035,-0.01100000032));
#7749=CARTESIAN_POINT('',(0.,-0.0180515951329767,0.00699377303329588));
#7750=CARTESIAN_POINT('',(0.00223898065795594,-0.0303403406237614,0.00699377303329588));
#7751=CARTESIAN_POINT('',(0.0114910488,-0.0180515951329767,0.00699377303329588));
#7752=CARTESIAN_POINT('',(0.0114910488,-0.0180515951329767,0.00725794733936277));
#7753=CARTESIAN_POINT('',(0.0117067049972431,-0.0180455852288112,0.00777558982005119));
#7754=CARTESIAN_POINT('',(0.0122306785725225,-0.0180305482603787,0.00799377303329574));
#7755=CARTESIAN_POINT('',(0.0124910159490166,-0.0180229475260995,0.00799377303329588));
#7756=CARTESIAN_POINT('',(0.00857740346184122,0.0516517948789017,0.00699377303329589));
#7757=CARTESIAN_POINT('',(0.008207892,0.0403990320215515,0.00699377303329589));
#7758=CARTESIAN_POINT('',(0.008207892,0.0403990320215515,0.00725794661302549));
#7759=CARTESIAN_POINT('',(0.00842354776978831,0.0404050261404905,0.00777558759299344));
#7760=CARTESIAN_POINT('',(0.008947512890695,0.0404201914761739,0.00799377303329587));
#7761=CARTESIAN_POINT('',(0.00920784674600956,0.0404279004413884,0.00799377303329589));
#7762=CARTESIAN_POINT('',(-0.00223898065795594,-0.0303403406237614,0.00799377303329588));
#7763=CARTESIAN_POINT('',(-0.00205973384739541,-0.029356536486291,0.00799377303329588));
#7764=CARTESIAN_POINT('',(-0.00205973384739541,-0.029356536486291,0.00699377303329588));
#7765=CARTESIAN_POINT('',(-0.000748242919122951,-0.0305797097356955,0.00799377303329588));
#7766=CARTESIAN_POINT('',(-0.000715497284706645,-0.0296014532411807,0.00796255052794581));
#7767=CARTESIAN_POINT('',(-0.000686577949433335,-0.0296067222760611,0.00699377303680561));
#7768=CARTESIAN_POINT('',(0.00074824291912353,-0.0305797097356876,0.00799377303329588));
#7769=CARTESIAN_POINT('',(0.000715497284696222,-0.0296014532411735,0.00796255052796054));
#7770=CARTESIAN_POINT('',(0.000686577949435276,-0.0296067222760607,0.00699377303680561));
#7771=CARTESIAN_POINT('',(0.00223898065795595,-0.0303403406237614,0.00799377303329588));
#7772=CARTESIAN_POINT('',(0.00205973384739542,-0.029356536486291,0.00799377303329588));
#7773=CARTESIAN_POINT('',(0.00205973384739542,-0.029356536486291,0.00699377303329588));
#7774=CARTESIAN_POINT('',(-0.00223898065795594,-0.0303403406237614,0.00699377303329588));
#7775=CARTESIAN_POINT('',(0.,0.0403990320215515,0.00699377303329589));
#7776=CARTESIAN_POINT('',(0.0070565442830717,0.0463143052920532,0.00699377303329589));
#7777=CARTESIAN_POINT('',(0.,-0.0180515951329767,0.00699377303329588));
#7778=CARTESIAN_POINT('',(-0.0114910488,-0.0180515951329767,0.00699377303329588));
#7779=CARTESIAN_POINT('',(-0.0114910488,-0.0180515951329767,0.00725794733936284));
#7780=CARTESIAN_POINT('',(-0.0117067049972432,-0.0180455852288116,0.00777558982005139));
#7781=CARTESIAN_POINT('',(-0.0122306785725228,-0.0180305482603778,0.00799377303329584));
#7782=CARTESIAN_POINT('',(-0.012491015949017,-0.0180229475260996,0.00799377303329588));
#7783=CARTESIAN_POINT('',(0.0070565442830717,0.0463143052920532,0.00799377303329589));
#7784=CARTESIAN_POINT('',(0.00629018600225436,0.0456718918851082,0.0079937730332959));
#7785=CARTESIAN_POINT('',(0.00629018600225436,0.0456718918851082,0.00699377303329589));
#7786=CARTESIAN_POINT('',(0.00663675715233699,0.0467813119196925,0.00799377303329589));
#7787=CARTESIAN_POINT('',(0.00593832363413206,0.0460916412822597,0.00797230984445771));
#7788=CARTESIAN_POINT('',(0.00590046854092382,0.0461367999963664,0.00699377303733907));
#7789=CARTESIAN_POINT('',(0.00569956743993915,0.0476010156616633,0.00809040380897171));
#7790=CARTESIAN_POINT('',(0.00516716899465536,0.0468516022761816,0.00800170584891698));
#7791=CARTESIAN_POINT('',(0.00503969845558102,0.0469583719208734,0.00710006688468222));
#7792=CARTESIAN_POINT('',(0.00343035019733497,0.0488224570843953,0.00851824659842775));
#7793=CARTESIAN_POINT('',(0.00322701332654366,0.0481104007221627,0.00828757882417505));
#7794=CARTESIAN_POINT('',(0.00299842737141029,0.0482019239037006,0.00757069395613992));
#7795=CARTESIAN_POINT('',(0.00140299443024176,0.0492029057968742,0.00882198790030551));
#7796=CARTESIAN_POINT('',(0.00128861423873263,0.0486014138339194,0.00856090079418309));
#7797=CARTESIAN_POINT('',(0.00122463996232749,0.0486019331129098,0.00790480938658279));
#7798=CARTESIAN_POINT('',(3.88600902680932E-5,0.0492076213378734,0.00882524260713517));
#7799=CARTESIAN_POINT('',(3.56761871683841E-5,0.048606846674528,0.00856365092865193));
#7800=CARTESIAN_POINT('',(3.39199894498218E-5,0.0486068539322645,0.00790838956451909));
#7801=CARTESIAN_POINT('',(7.73286032330566E-5,0.0486066725565947,0.00790817556294355));
#7802=CARTESIAN_POINT('',(7.79535025252851E-5,0.0486066544098561,0.00803061290174059));
#7803=CARTESIAN_POINT('',(8.0300967418879E-5,0.0486475761391194,0.00835362636492919));
#7804=CARTESIAN_POINT('',(8.48436697596153E-5,0.0489649915149441,0.00871960415239467));
#7805=CARTESIAN_POINT('',(8.76638406754314E-5,0.0492072689642466,0.00882517851789361));
#7806=CARTESIAN_POINT('',(-0.0114425698213259,0.000642726224631286,0.00699377303329588));
#7807=CARTESIAN_POINT('',(-0.008207892,0.0403990320215515,0.00699377303329589));
#7808=CARTESIAN_POINT('',(-0.008207892,0.0403990320215515,0.00725794661302554));
#7809=CARTESIAN_POINT('',(-0.00842354776978844,0.0404050261404894,0.0077755875929936));
#7810=CARTESIAN_POINT('',(-0.0089475128906952,0.0404201914761762,0.00799377303329595));
#7811=CARTESIAN_POINT('',(-0.00920784674600988,0.0404279004413884,0.00799377303329589));
#7812=CARTESIAN_POINT('',(-5.61597199378756E-9,0.0496067442138064,0.00790829977384746));
#7813=CARTESIAN_POINT('',(-8.76638410861103E-5,0.0492072689878249,0.00882517846382129));
#7814=CARTESIAN_POINT('',(-8.48436494395307E-5,0.0489649897645646,0.00871960336263682));
#7815=CARTESIAN_POINT('',(-8.03009008679873E-5,0.0486475743651198,0.00835362258293446));
#7816=CARTESIAN_POINT('',(-7.79534925679463E-5,0.0486066543685292,0.00803061098119678));
#7817=CARTESIAN_POINT('',(-7.73286030826419E-5,0.0486066725101695,0.00790817556293302));
#7818=CARTESIAN_POINT('',(0.,0.0403990320215515,0.00699377303329589));
#7819=CARTESIAN_POINT('',(-0.0070565442830717,0.0463143052920532,0.00699377303329589));
#7820=CARTESIAN_POINT('',(-0.00629018600225436,0.0456718918851082,0.00699377303329589));
#7821=CARTESIAN_POINT('',(-0.00629018600225436,0.0456718918851082,0.0079937730332959));
#7822=CARTESIAN_POINT('',(-0.0070565442830717,0.0463143052920532,0.00799377303329589));
#7823=CARTESIAN_POINT('',(-0.00590046854092381,0.0461367999963664,0.00699377303733907));
#7824=CARTESIAN_POINT('',(-0.00593832363413165,0.0460916412822597,0.00797230984445853));
#7825=CARTESIAN_POINT('',(-0.00663675715233699,0.0467813119196925,0.00799377303329589));
#7826=CARTESIAN_POINT('',(-0.00503969845558102,0.0469583719208734,0.00710006688468207));
#7827=CARTESIAN_POINT('',(-0.00516716899465555,0.0468516022761816,0.0080017058489165));
#7828=CARTESIAN_POINT('',(-0.00569956743993915,0.0476010156616632,0.00809040380897169));
#7829=CARTESIAN_POINT('',(-0.00299842737141019,0.0482019239037006,0.00757069395614071));
#7830=CARTESIAN_POINT('',(-0.00322701332654346,0.0481104007221627,0.00828757882417575));
#7831=CARTESIAN_POINT('',(-0.00343035019733485,0.0488224570843956,0.00851824659842788));
#7832=CARTESIAN_POINT('',(-0.00122463996232772,0.0486019331129098,0.00790480938657932));
#7833=CARTESIAN_POINT('',(-0.00128861423873286,0.0486014138339194,0.00856090079418102));
#7834=CARTESIAN_POINT('',(-0.00140299443024203,0.049202905796873,0.00882198790030496));
#7835=CARTESIAN_POINT('',(-3.39199894497602E-5,0.0486068539322645,0.00790838956451909));
#7836=CARTESIAN_POINT('',(-3.56761871683194E-5,0.048606846674528,0.00856365092865193));
#7837=CARTESIAN_POINT('',(-3.88600902680227E-5,0.0492076213378734,0.00882524260713517));
#7838=CARTESIAN_POINT('',(0.0479406149651572,-0.0267770382679513,0.0100000004));
#7839=CARTESIAN_POINT('',(0.0200162970866488,-0.0452885101813074,0.0100000004));
#7840=CARTESIAN_POINT('',(0.03550000008,-0.0578844846861028,0.0100000004));
#7841=CARTESIAN_POINT('',(0.0150966619928104,-0.0333889120212244,0.00799377303329588));
#7842=CARTESIAN_POINT('',(0.0160769945899842,-0.0331915595474162,0.00799377303329574));
#7843=CARTESIAN_POINT('',(0.0160769945899843,-0.0331915595474164,0.00699377303329588));
#7844=CARTESIAN_POINT('',(0.0156068158482343,-0.0354384287074729,0.00799377303329628));
#7845=CARTESIAN_POINT('',(0.0164617445111704,-0.0351027739527766,0.00790249484173019));
#7846=CARTESIAN_POINT('',(0.016507408986648,-0.0353296085680356,0.0069937730392069));
#7847=CARTESIAN_POINT('',(0.0170663475656315,-0.039383215844924,0.00882366076850159));
#7848=CARTESIAN_POINT('',(0.0175691716233034,-0.0389007355739478,0.00846666609668826));
#7849=CARTESIAN_POINT('',(0.0177790331975587,-0.0394032662983737,0.0079066495412027));
#7850=CARTESIAN_POINT('',(0.0192020228605085,-0.0429774328463579,0.0102276505555518));
#7851=CARTESIAN_POINT('',(0.0195815577937507,-0.0428095980046108,0.00992665585498373));
#7852=CARTESIAN_POINT('',(0.0196915521790964,-0.0429887931416397,0.00945103830350577));
#7853=CARTESIAN_POINT('',(0.0204657792849938,-0.0447690265275819,0.0107267070030269));
#7854=CARTESIAN_POINT('',(0.0207883947143824,-0.0446433660335932,0.0104373351105851));
#7855=CARTESIAN_POINT('',(0.0208497874735457,-0.04473597622312,0.0100000004));
#7856=CARTESIAN_POINT('',(0.0200162970866488,-0.0452885101813074,0.0100000004));
#7857=CARTESIAN_POINT('',(0.0150966619928104,-0.033388912021225,0.00699377303329588));
#7858=CARTESIAN_POINT('',(0.0479406149651572,-0.0267770382679513,0.00699377303329588));
#7859=CARTESIAN_POINT('',(0.0144904743180211,-0.028655924125519,0.00699377303329588));
#7860=CARTESIAN_POINT('',(0.00997520014598791,0.0517303087616774,0.00699377303329589));
#7861=CARTESIAN_POINT('',(0.0106041148871086,0.0405336272491669,0.00699377303329589));
#7862=CARTESIAN_POINT('',(0.0770011542117716,0.0442631319913884,0.00699377303329589));
#7863=CARTESIAN_POINT('',(0.0105921890504172,0.0477738844607486,0.00699377303329589));
#7864=CARTESIAN_POINT('',(0.0115907945846862,0.0477210925397055,0.00699377303329589));
#7865=CARTESIAN_POINT('',(0.0115907945846862,0.0477210925397055,0.00799377303329589));
#7866=CARTESIAN_POINT('',(0.0105921890504172,0.0477738844607486,0.00799377303329589));
#7867=CARTESIAN_POINT('',(0.0116515412207203,0.0488701684917309,0.00699377303595376));
#7868=CARTESIAN_POINT('',(0.0116460760642758,0.0487667902637238,0.0079486554524551));
#7869=CARTESIAN_POINT('',(0.0106957683040226,0.0488588221723761,0.00799377303329589));
#7870=CARTESIAN_POINT('',(0.0118303126054586,0.0511152954428151,0.00726680033959949));
#7871=CARTESIAN_POINT('',(0.0118031703322206,0.0508361592339147,0.00808736980035808));
#7872=CARTESIAN_POINT('',(0.0109685466035936,0.0509905050542671,0.00824197967638395));
#7873=CARTESIAN_POINT('',(0.012258993120378,0.0543814318068636,0.00828727294311878));
#7874=CARTESIAN_POINT('',(0.0122076213027949,0.054049654560765,0.008901337887955));
#7875=CARTESIAN_POINT('',(0.0115702429201356,0.0541479034369561,0.0091696820423716));
#7876=CARTESIAN_POINT('',(0.0128211649345827,0.0574770135698663,0.00966421320591958));
#7877=CARTESIAN_POINT('',(0.0127613931441757,0.0571911655523929,0.0101117586977671));
#7878=CARTESIAN_POINT('',(0.0123263746292134,0.057221859950959,0.0104214459159221));
#7879=CARTESIAN_POINT('',(0.0132893215582609,0.0595090645092564,0.0106162645373174));
#7880=CARTESIAN_POINT('',(0.0132467806557497,0.0593347911247093,0.0110069763063105));
#7881=CARTESIAN_POINT('',(0.0129239618696705,0.0593100555036904,0.0112869471314436));
#7882=CARTESIAN_POINT('',(0.0135575831556229,0.0605538020003774,0.0110000003200065));
#7883=CARTESIAN_POINT('',(0.0135257202877438,0.0604297129284592,0.0113656106861467));
#7884=CARTESIAN_POINT('',(0.0132493773070656,0.0604029222734306,0.0116357978393965));
#7885=CARTESIAN_POINT('',(0.0125890041486941,0.0608025080665215,0.0110000003200065));
#7886=CARTESIAN_POINT('',(-0.0479406149651572,-0.0267770382679513,0.0100000004));
#7887=CARTESIAN_POINT('',(-0.0200162970866488,-0.0452885101813074,0.0100000004));
#7888=CARTESIAN_POINT('',(-0.03550000008,-0.0578844846861028,0.0100000004));
#7889=CARTESIAN_POINT('',(-0.0160769945899836,-0.0331915595474134,0.00699377303329588));
#7890=CARTESIAN_POINT('',(-0.0160769945899836,-0.0331915595474134,0.00799377303329588));
#7891=CARTESIAN_POINT('',(-0.0150966619928097,-0.0333889120212214,0.00799377303329588));
#7892=CARTESIAN_POINT('',(-0.0165074089866394,-0.0353296085679943,0.00699377303920885));
#7893=CARTESIAN_POINT('',(-0.0164617445112181,-0.0351027739527186,0.0079024948417222));
#7894=CARTESIAN_POINT('',(-0.0156068158483019,-0.0354384287074471,0.00799377303329588));
#7895=CARTESIAN_POINT('',(-0.0177790331975661,-0.0394032662983982,0.00790664954120865));
#7896=CARTESIAN_POINT('',(-0.0175691716232746,-0.0389007355739849,0.00846666609669959));
#7897=CARTESIAN_POINT('',(-0.0170663475655921,-0.0393832158449445,0.00882366076851098));
#7898=CARTESIAN_POINT('',(-0.0196915521790878,-0.0429887931416268,0.00945103830349017));
#7899=CARTESIAN_POINT('',(-0.0195815577937629,-0.0428095980045893,0.00992665585496803));
#7900=CARTESIAN_POINT('',(-0.0192020228605171,-0.0429774328463374,0.0102276505555318));
#7901=CARTESIAN_POINT('',(-0.0208497874735458,-0.04473597622312,0.0100000004));
#7902=CARTESIAN_POINT('',(-0.0207883947143824,-0.0446433660335932,0.0104373351105851));
#7903=CARTESIAN_POINT('',(-0.0204657792849938,-0.0447690265275819,0.0107267070030269));
#7904=CARTESIAN_POINT('',(-0.0200162970866488,-0.0452885101813074,0.0100000004));
#7905=CARTESIAN_POINT('',(-0.0150966619928097,-0.0333889120212214,0.00699377303329588));
#7906=CARTESIAN_POINT('',(-0.0479406149651572,-0.0267770382679513,0.00699377303329588));
#7907=CARTESIAN_POINT('',(-0.0144904743180211,-0.028655924125519,0.00699377303329588));
#7908=CARTESIAN_POINT('',(-0.0128403665054726,0.00072124010740693,0.00699377303329588));
#7909=CARTESIAN_POINT('',(-0.0106041148871086,0.0405336272491669,0.00699377303329589));
#7910=CARTESIAN_POINT('',(-0.0770011542117716,0.0442631319913884,0.00699377303329589));
#7911=CARTESIAN_POINT('',(-0.0105921890504174,0.0477738844607517,0.00699377303329589));
#7912=CARTESIAN_POINT('',(-0.0105921890504175,0.0477738844607515,0.00799377303329589));
#7913=CARTESIAN_POINT('',(-0.0115907945846863,0.0477210925397084,0.00799377303329577));
#7914=CARTESIAN_POINT('',(-0.0115907945846864,0.0477210925397086,0.00699377303329589));
#7915=CARTESIAN_POINT('',(-0.0106957683040308,0.0488588221723772,0.00799377303329611));
#7916=CARTESIAN_POINT('',(-0.0116460760642879,0.0487667902636878,0.00794865545245672));
#7917=CARTESIAN_POINT('',(-0.0116515412207195,0.0488701684917165,0.00699377303595376));
#7918=CARTESIAN_POINT('',(-0.0109685466035879,0.0509905050542611,0.00824197967638324));
#7919=CARTESIAN_POINT('',(-0.0118031703322129,0.0508361592339223,0.00808736980035708));
#7920=CARTESIAN_POINT('',(-0.011830312605458,0.0511152954428164,0.007266800339599));
#7921=CARTESIAN_POINT('',(-0.011570242920141,0.0541479034369613,0.00916968204237088));
#7922=CARTESIAN_POINT('',(-0.012207621302802,0.0540496545607705,0.00890133788795375));
#7923=CARTESIAN_POINT('',(-0.0122589931203798,0.054381431806866,0.00828727294311737));
#7924=CARTESIAN_POINT('',(-0.0123263746291878,0.0572218599508996,0.0104214459159101));
#7925=CARTESIAN_POINT('',(-0.0127613931441502,0.0571911655523285,0.0101117586977604));
#7926=CARTESIAN_POINT('',(-0.0128211649345689,0.05747701356981,0.00966421320590858));
#7927=CARTESIAN_POINT('',(-0.0129239618697132,0.0593100555037755,0.0112869471314516));
#7928=CARTESIAN_POINT('',(-0.0132467806557926,0.0593347911248004,0.0110069763063061));
#7929=CARTESIAN_POINT('',(-0.0132893215582819,0.0595090645093368,0.0106162645373216));
#7930=CARTESIAN_POINT('',(-0.0132493773070601,0.060402922273412,0.0116357978393905));
#7931=CARTESIAN_POINT('',(-0.0135257202877391,0.0604297129284408,0.0113656106861407));
#7932=CARTESIAN_POINT('',(-0.0135575831556184,0.0605538020003596,0.01100000032));
#7933=CARTESIAN_POINT('',(-0.0125890041486895,0.0608025080665035,0.01100000032));
#7934=CARTESIAN_POINT('',(0.,0.0403990320215515,-0.0026));
#7935=CARTESIAN_POINT('',(0.008207892,0.0403990320215515,-0.0026));
#7936=CARTESIAN_POINT('',(0.008207892,0.0403990320215515,-0.00233582041202306));
#7937=CARTESIAN_POINT('',(0.0079922321936474,0.0403929152387221,-0.001818166590201));
#7938=CARTESIAN_POINT('',(0.00746820258969384,0.0403787024449851,-0.00160000000000006));
#7939=CARTESIAN_POINT('',(0.00720784085825546,0.0403718797522114,-0.0016));
#7940=CARTESIAN_POINT('',(-0.008207892,0.0403990320215515,-0.0026));
#7941=CARTESIAN_POINT('',(-0.008207892,0.0403990320215515,-0.00233582041202305));
#7942=CARTESIAN_POINT('',(-0.00799223219364738,0.0403929152387224,-0.00181816659020097));
#7943=CARTESIAN_POINT('',(-0.0074682025896938,0.0403787024449846,-0.00160000000000004));
#7944=CARTESIAN_POINT('',(-0.0072078408582554,0.0403718797522114,-0.0016));
#7945=CARTESIAN_POINT('',(-0.00944571741540203,0.000530563534951791,-0.0026));
#7946=CARTESIAN_POINT('',(-0.0114910488,-0.0180515951329767,-0.0026));
#7947=CARTESIAN_POINT('',(-0.0114910488,-0.0180515951329767,-0.00233582142178957));
#7948=CARTESIAN_POINT('',(-0.0112753897480323,-0.0180576927166228,-0.00181816981976291));
#7949=CARTESIAN_POINT('',(-0.010751370193641,-0.0180720491888478,-0.00159999999999997));
#7950=CARTESIAN_POINT('',(-0.0104910129546955,-0.018079019727579,-0.0016));
#7951=CARTESIAN_POINT('',(0.00944571741540203,0.000530563534951791,-0.0026));
#7952=CARTESIAN_POINT('',(0.0114910488,-0.0180515951329767,-0.0026));
#7953=CARTESIAN_POINT('',(0.0114910488,-0.0180515951329767,-0.00233582142178957));
#7954=CARTESIAN_POINT('',(0.0112753897480323,-0.018057692716622,-0.00181816981976291));
#7955=CARTESIAN_POINT('',(0.010751370193641,-0.0180720491888493,-0.00159999999999997));
#7956=CARTESIAN_POINT('',(0.0104910129546955,-0.018079019727579,-0.0016));
#7957=CARTESIAN_POINT('',(0.,-0.0180515951329767,-0.0026));
#7958=CARTESIAN_POINT('',(-0.0200162970866488,-0.0452885101813074,0.0100000004));
#7959=CARTESIAN_POINT('',(-0.0200162970866488,-0.0452885101813074,0.0100000004));
#7960=CARTESIAN_POINT('',(0.,-0.0684221052,0.0100000004));
#7961=CARTESIAN_POINT('',(0.0200162970866488,-0.0452885101813074,0.0100000004));
#7962=CARTESIAN_POINT('',(0.0200162970866488,-0.0452885101813074,0.0100000004));
#7963=CARTESIAN_POINT('',(-0.03550000008,-0.0578844846861027,-0.0100000004));
#7964=CARTESIAN_POINT('',(-0.03550000008,-0.0578844846861028,-0.0100000004));
#7965=CARTESIAN_POINT('',(-0.03550000008,-0.0578844846861027,-0.01200000032));
#7966=CARTESIAN_POINT('',(-0.03550000008,-0.0578844846861027,0.0100000004));
#7967=CARTESIAN_POINT('',(-0.03550000008,-0.0578844846861027,0.0100000004));
#7968=CARTESIAN_POINT('',(0.03550000008,-0.0578844846861027,-0.0100000004));
#7969=CARTESIAN_POINT('',(0.03550000008,-0.0578844846861027,-0.0100000004));
#7970=CARTESIAN_POINT('',(0.03550000008,-0.0578844846861027,-0.01200000032));
#7971=CARTESIAN_POINT('',(0.03550000008,-0.0578844846861027,0.0100000004));
#7972=CARTESIAN_POINT('',(0.03550000008,-0.0578844846861027,0.0100000004));
#7973=CARTESIAN_POINT('',(0.0200162970866488,-0.0452885101813074,-0.0100000004));
#7974=CARTESIAN_POINT('',(0.0200162970866488,-0.0452885101813074,-0.0100000004));
#7975=CARTESIAN_POINT('',(0.,-0.0684221052,-0.0100000004));
#7976=CARTESIAN_POINT('',(-0.0200162970866503,-0.0452885101813087,-0.0100000004));
#7977=CARTESIAN_POINT('',(-0.0200162970866488,-0.0452885101813074,-0.0100000004));
#7978=CARTESIAN_POINT('',(0.,0.06842,-0.01100000032));
#7979=CARTESIAN_POINT('',(-0.0135487072274815,0.0641694879715509,-0.01100000032));
#7980=CARTESIAN_POINT('',(0.0135487072274815,0.0641694879715509,-0.01100000032));
#7981=CARTESIAN_POINT('',(0.0770011542117716,0.0442631319913884,-0.01100000032));
#7982=CARTESIAN_POINT('',(0.0125890041486895,0.0608025080665035,-0.01100000032));
#7983=CARTESIAN_POINT('',(-0.0770011542117716,0.0442631319913884,-0.01100000032));
#7984=CARTESIAN_POINT('',(-0.0125890041486895,0.0608025080665034,-0.01100000032));
#7985=CARTESIAN_POINT('',(0.0125890041486895,0.0608025080665035,-0.01100000032));
#7986=CARTESIAN_POINT('',(0.0125890041486895,0.0608025080665035,-0.01100000032));
#7987=CARTESIAN_POINT('',(-0.0125890041486895,0.0608025080665034,-0.01100000032));
#7988=CARTESIAN_POINT('',(-0.0125890041486895,0.0608025080665034,-0.01100000032));
#7989=CARTESIAN_POINT('',(0.,0.06842,-0.01100000032));
#7990=CARTESIAN_POINT('',(7.87045304645721E-5,0.0529340922159572,-0.0116357978393905));
#7991=CARTESIAN_POINT('',(7.82254313897608E-5,0.0531226285545892,-0.0118646802727782));
#7992=CARTESIAN_POINT('',(7.74797395333406E-5,0.0534133411399295,-0.01200000032));
#7993=CARTESIAN_POINT('',(7.67180601915171E-5,0.0537059481055745,-0.01200000032));
#7994=CARTESIAN_POINT('',(0.,0.06842,-0.01100000032));
#7995=CARTESIAN_POINT('',(-7.87045304645737E-5,0.0529340922159572,-0.0116357978393905));
#7996=CARTESIAN_POINT('',(-7.82254313897624E-5,0.0531226285545892,-0.0118646802727782));
#7997=CARTESIAN_POINT('',(-7.74797395310902E-5,0.0534133411399295,-0.01200000032));
#7998=CARTESIAN_POINT('',(-7.67180601914596E-5,0.0537059481055745,-0.01200000032));
#7999=CARTESIAN_POINT('',(0.03650000008,0.0537059481055745,-0.01100000032));
#8000=CARTESIAN_POINT('',(0.,0.06842,-0.01300000032));
#8001=CARTESIAN_POINT('',(0.,0.06842,-0.0120000004));
#8002=CARTESIAN_POINT('',(0.,0.06842,0.0120000004));
#8003=CARTESIAN_POINT('',(0.,0.06842,0.01100000032));
#8004=CARTESIAN_POINT('',(-0.0135487072274815,0.0641694879715509,0.01100000032));
#8005=CARTESIAN_POINT('',(0.0135487072274815,0.0641694879715509,0.01100000032));
#8006=CARTESIAN_POINT('',(0.0770011542117716,0.0442631319913884,0.01100000032));
#8007=CARTESIAN_POINT('',(0.0125890041486819,0.060802508066474,0.01100000032));
#8008=CARTESIAN_POINT('',(-0.0770011542117716,0.0442631319913884,0.01100000032));
#8009=CARTESIAN_POINT('',(-0.0125890041486895,0.0608025080665035,0.01100000032));
#8010=CARTESIAN_POINT('',(0.0125890041486895,0.0608025080665034,0.01100000032));
#8011=CARTESIAN_POINT('',(0.0125890041486895,0.0608025080665034,0.01100000032));
#8012=CARTESIAN_POINT('',(-0.0125890041486895,0.0608025080665035,0.01100000032));
#8013=CARTESIAN_POINT('',(-0.0125890041486895,0.0608025080665035,0.01100000032));
#8014=CARTESIAN_POINT('',(0.,0.06842,0.01100000032));
#8015=CARTESIAN_POINT('',(7.87045304634033E-5,0.0529340922159572,0.0116357978393905));
#8016=CARTESIAN_POINT('',(7.82254313883414E-5,0.0531226285545892,0.0118646802727782));
#8017=CARTESIAN_POINT('',(7.74797395308895E-5,0.0534133411399295,0.01200000032));
#8018=CARTESIAN_POINT('',(7.67180601909946E-5,0.0537059481055745,0.01200000032));
#8019=CARTESIAN_POINT('',(0.,0.06842,0.01100000032));
#8020=CARTESIAN_POINT('',(-7.87045304634164E-5,0.0529340922159572,0.0116357978393905));
#8021=CARTESIAN_POINT('',(-7.82254313883546E-5,0.0531226285545892,0.0118646802727782));
#8022=CARTESIAN_POINT('',(-7.74797395313073E-5,0.0534133411399295,0.01200000032));
#8023=CARTESIAN_POINT('',(-7.67180601908343E-5,0.0537059481055745,0.01200000032));
#8024=CARTESIAN_POINT('',(0.03650000008,0.0537059481055745,0.01100000032));
#8025=CARTESIAN_POINT('',(0.,0.06842,0.01300000032));
#8026=CARTESIAN_POINT('',(0.0434268042445183,-0.0746532949430514,0.0110000004));
#8027=CARTESIAN_POINT('',(0.0434268042445183,-0.0746532949430514,0.0110000004));
#8534=MECHANICAL_DESIGN_GEOMETRIC_PRESENTATION_REPRESENTATION('',(#4340),#8535);
#8535=(
GEOMETRIC_REPRESENTATION_CONTEXT(3)
GLOBAL_UNCERTAINTY_ASSIGNED_CONTEXT((#8547))
GLOBAL_UNIT_ASSIGNED_CONTEXT((#8561,#8560,#8559))
REPRESENTATION_CONTEXT('MAS-680','TOP_LEVEL_ASSEMBLY_PART')
);
#8542=(
GEOMETRIC_REPRESENTATION_CONTEXT(3)
GLOBAL_UNCERTAINTY_ASSIGNED_CONTEXT((#8554))
GLOBAL_UNIT_ASSIGNED_CONTEXT((#8561,#8560,#8559))
REPRESENTATION_CONTEXT('Part 1','COMPONENT_PART')
);
#8547=UNCERTAINTY_MEASURE_WITH_UNIT(LENGTH_MEASURE(1.E-8),#8561,
'DISTANCE_ACCURACY_VALUE','Maximum Tolerance applied to model');
#8554=UNCERTAINTY_MEASURE_WITH_UNIT(LENGTH_MEASURE(2.E-5),#8561,
'DISTANCE_ACCURACY_VALUE','Maximum Tolerance applied to model');
#8559=(
NAMED_UNIT(*)
SI_UNIT($,.STERADIAN.)
SOLID_ANGLE_UNIT()
);
#8560=(
NAMED_UNIT(*)
PLANE_ANGLE_UNIT()
SI_UNIT($,.RADIAN.)
);
#8561=(
LENGTH_UNIT()
NAMED_UNIT(*)
SI_UNIT($,.METRE.)
);
#8578=PRODUCT_DEFINITION_SHAPE('','',#8596);
#8596=PRODUCT_DEFINITION('','',#8620,#8608);
#8608=PRODUCT_DEFINITION_CONTEXT('',#8674,'design');
#8620=PRODUCT_DEFINITION_FORMATION_WITH_SPECIFIED_SOURCE('','',#8644,
 .NOT_KNOWN.);
#8644=PRODUCT('Part 1','Part 1','Part 1',(#8668));
#8668=PRODUCT_CONTEXT('',#8674,'mechanical');
#8674=APPLICATION_CONTEXT('managed model based 3d engineering');
ENDSEC;
END-ISO-10303-21;
